ISO-10303-21;
HEADER;
/* Generated by software containing ST-Developer
 * from STEP Tools, Inc. (www.steptools.com) 
 */

FILE_DESCRIPTION(
/* description */ (''),
/* implementation_level */ '2;1');

FILE_NAME(
/* name */ 'Hex nut M3.step',
/* time_stamp */ '2026-11-10T08:27:36-08:00',
/* author */ (''),
/* organization */ (''),
/* preprocessor_version */ 'ST-DEVELOPER v20.2',
/* originating_system */ 'Autodesk Translation Framework v15.17.0.0',
/* authorisation */ '');

FILE_SCHEMA (('AUTOMOTIVE_DESIGN { 1 0 10303 214 3 1 1 }'));
ENDSEC;

DATA;
#10=MECHANICAL_DESIGN_GEOMETRIC_PRESENTATION_REPRESENTATION('',(#574),#19090);
#170=B_SPLINE_SURFACE_WITH_KNOTS('',3,3,((#18461,#18462,#18463,#18464,#18465,
#18466,#18467,#18468,#18469,#18470,#18471,#18472,#18473,#18474,#18475,#18476,
#18477,#18478,#18479,#18480,#18481,#18482,#18483,#18484,#18485,#18486,#18487,
#18488,#18489,#18490,#18491,#18492,#18493,#18494,#18495,#18496),(#18497,
#18498,#18499,#18500,#18501,#18502,#18503,#18504,#18505,#18506,#18507,#18508,
#18509,#18510,#18511,#18512,#18513,#18514,#18515,#18516,#18517,#18518,#18519,
#18520,#18521,#18522,#18523,#18524,#18525,#18526,#18527,#18528,#18529,#18530,
#18531,#18532),(#18533,#18534,#18535,#18536,#18537,#18538,#18539,#18540,
#18541,#18542,#18543,#18544,#18545,#18546,#18547,#18548,#18549,#18550,#18551,
#18552,#18553,#18554,#18555,#18556,#18557,#18558,#18559,#18560,#18561,#18562,
#18563,#18564,#18565,#18566,#18567,#18568),(#18569,#18570,#18571,#18572,
#18573,#18574,#18575,#18576,#18577,#18578,#18579,#18580,#18581,#18582,#18583,
#18584,#18585,#18586,#18587,#18588,#18589,#18590,#18591,#18592,#18593,#18594,
#18595,#18596,#18597,#18598,#18599,#18600,#18601,#18602,#18603,#18604)),
 .UNSPECIFIED.,.F.,.F.,.F.,(4,4),(4,1,1,1,1,1,1,1,1,1,1,1,1,1,1,1,1,1,1,
1,1,1,1,1,1,1,1,1,1,1,1,1,1,4),(0.,0.0321584099938622),(11.8553612635794,
12.830508595889,13.8056559281987,14.7808032605084,15.755950592818,16.7310979251277,
17.7062452574374,18.681392589747,19.6565399220567,20.6316872543664,21.606834586676,
22.5819819189857,23.5571292512954,24.532276583605,25.5074239159147,26.4825712482243,
27.457718580534,28.4328659128437,29.4080132451533,30.383160577463,31.3583079097727,
32.3334552420823,33.308602574392,34.2837499067017,35.2588972390113,36.234044571321,
37.2091919036307,38.1843392359403,39.15948656825,40.1346339005596,41.1097812328693,
42.084928565179,43.0600758974886,44.0352232297983),.UNSPECIFIED.);
#171=B_SPLINE_SURFACE_WITH_KNOTS('',3,3,((#18728,#18729,#18730,#18731,#18732,
#18733,#18734,#18735,#18736,#18737,#18738,#18739,#18740,#18741,#18742,#18743,
#18744,#18745,#18746,#18747,#18748,#18749,#18750,#18751,#18752,#18753,#18754,
#18755,#18756,#18757,#18758,#18759,#18760,#18761,#18762,#18763),(#18764,
#18765,#18766,#18767,#18768,#18769,#18770,#18771,#18772,#18773,#18774,#18775,
#18776,#18777,#18778,#18779,#18780,#18781,#18782,#18783,#18784,#18785,#18786,
#18787,#18788,#18789,#18790,#18791,#18792,#18793,#18794,#18795,#18796,#18797,
#18798,#18799),(#18800,#18801,#18802,#18803,#18804,#18805,#18806,#18807,
#18808,#18809,#18810,#18811,#18812,#18813,#18814,#18815,#18816,#18817,#18818,
#18819,#18820,#18821,#18822,#18823,#18824,#18825,#18826,#18827,#18828,#18829,
#18830,#18831,#18832,#18833,#18834,#18835),(#18836,#18837,#18838,#18839,
#18840,#18841,#18842,#18843,#18844,#18845,#18846,#18847,#18848,#18849,#18850,
#18851,#18852,#18853,#18854,#18855,#18856,#18857,#18858,#18859,#18860,#18861,
#18862,#18863,#18864,#18865,#18866,#18867,#18868,#18869,#18870,#18871)),
 .UNSPECIFIED.,.F.,.F.,.F.,(4,4),(4,1,1,1,1,1,1,1,1,1,1,1,1,1,1,1,1,1,1,
1,1,1,1,1,1,1,1,1,1,1,1,1,1,4),(0.,0.0321584099938622),(14.3984001269719,
15.3735474592815,16.3486947915912,17.3238421239009,18.2989894562105,19.2741367885202,
20.2492841208299,21.2244314531395,22.1995787854492,23.1747261177589,24.1498734500685,
25.1250207823782,26.1001681146879,27.0753154469975,28.0504627793072,29.0256101116168,
30.0007574439265,30.9759047762362,31.9510521085458,32.9261994408555,33.9013467731652,
34.8764941054748,35.8516414377845,36.8267887700942,37.8019361024038,38.7770834347135,
39.7522307670232,40.7273780993328,41.7025254316425,42.6776727639522,43.6528200962618,
44.6279674285715,45.6031147608811,46.5782620931908),.UNSPECIFIED.);
#519=B_SPLINE_CURVE_WITH_KNOTS('',3,(#18131,#18132,#18133,#18134,#18135,
#18136,#18137),.UNSPECIFIED.,.F.,.F.,(4,3,4),(-30.159289474462,-29.2544199692899,
-28.9853432330879),.UNSPECIFIED.);
#520=B_SPLINE_CURVE_WITH_KNOTS('',3,(#18143,#18144,#18145,#18146,#18147,
#18148,#18149,#18150,#18151,#18152,#18153,#18154,#18155,#18156,#18157,#18158,
#18159,#18160,#18161),.UNSPECIFIED.,.F.,.F.,(4,3,3,3,3,3,4),(26.4423043696954,
27.3041253046706,28.2792726369803,29.25441996929,30.2295673015996,31.2047146339093,
32.179861966219),.UNSPECIFIED.);
#521=B_SPLINE_CURVE_WITH_KNOTS('',3,(#18163,#18164,#18165,#18166,#18167,
#18168,#18169,#18170,#18171,#18172,#18173,#18174,#18175,#18176,#18177,#18178,
#18179,#18180,#18181,#18182,#18183,#18184),.UNSPECIFIED.,.F.,.F.,(4,3,3,
3,3,3,3,4),(-28.9853432330879,-28.2792726369803,-27.3041253046706,-26.3289779723609,
-25.3538306400513,-24.3786833077416,-23.403535975432,-22.7021579259084),
 .UNSPECIFIED.);
#522=B_SPLINE_CURVE_WITH_KNOTS('',3,(#18189,#18190,#18191,#18192,#18193,
#18194,#18195,#18196,#18197,#18198,#18199,#18200,#18201,#18202,#18203,#18204,
#18205,#18206,#18207,#18208,#18209,#18210,#18211,#18212,#18213),
 .UNSPECIFIED.,.F.,.F.,(4,3,3,3,3,3,3,3,4),(20.1591190625159,20.478093978503,
21.4532413108126,22.4283886431223,23.403535975432,24.3786833077416,25.3538306400513,
26.328977972361,26.4423043696954),.UNSPECIFIED.);
#523=B_SPLINE_CURVE_WITH_KNOTS('',3,(#18214,#18215,#18216,#18217,#18218,
#18219,#18220,#18221,#18222,#18223,#18224,#18225,#18226,#18227,#18228,#18229,
#18230,#18231,#18232,#18233,#18234,#18235,#18236,#18237,#18238),
 .UNSPECIFIED.,.F.,.F.,(4,3,3,3,3,3,3,3,4),(-22.7021579259084,-22.4283886431223,
-21.4532413108126,-20.478093978503,-19.5029466461933,-18.5277993138836,
-17.552651981574,-16.5775046492643,-16.4189726187288),.UNSPECIFIED.);
#524=B_SPLINE_CURVE_WITH_KNOTS('',3,(#18243,#18244,#18245,#18246,#18247,
#18248,#18249,#18250,#18251,#18252,#18253,#18254,#18255,#18256,#18257,#18258,
#18259,#18260,#18261,#18262,#18263,#18264),.UNSPECIFIED.,.F.,.F.,(4,3,3,
3,3,3,3,4),(13.8759337553363,14.627209984645,15.6023573169546,16.5775046492643,
17.552651981574,18.5277993138836,19.5029466461933,20.1591190625159),
 .UNSPECIFIED.);
#525=B_SPLINE_CURVE_WITH_KNOTS('',3,(#18265,#18266,#18267,#18268,#18269,
#18270,#18271,#18272,#18273,#18274,#18275,#18276,#18277,#18278,#18279,#18280,
#18281,#18282,#18283,#18284,#18285,#18286),.UNSPECIFIED.,.F.,.F.,(4,3,3,
3,3,3,3,4),(-16.4189726187288,-15.6023573169546,-14.627209984645,-13.6520626523353,
-12.6769153200256,-11.701767987716,-10.7266206554063,-10.1357873115492),
 .UNSPECIFIED.);
#526=B_SPLINE_CURVE_WITH_KNOTS('',3,(#18292,#18293,#18294,#18295,#18296,
#18297,#18298,#18299,#18300,#18301,#18302,#18303,#18304),.UNSPECIFIED.,
 .F.,.F.,(4,3,3,3,4),(-3.8526020043696,-2.92544199692899,-1.95029466461933,
-0.975147332309664,0.),.UNSPECIFIED.);
#527=B_SPLINE_CURVE_WITH_KNOTS('',3,(#18307,#18308,#18309,#18310,#18311,
#18312,#18313,#18314,#18315,#18316,#18317,#18318,#18319,#18320,#18321,#18322,
#18323,#18324,#18325),.UNSPECIFIED.,.F.,.F.,(4,3,3,3,3,3,4),(2.02057249175693,
2.925441996929,3.90058932923866,4.87573666154832,5.85088399385799,6.82603132616766,
7.59274844815668),.UNSPECIFIED.);
#528=B_SPLINE_CURVE_WITH_KNOTS('',3,(#18331,#18332,#18333,#18334,#18335,
#18336,#18337),.UNSPECIFIED.,.F.,.F.,(4,1,1,1,4),(40.8407044966673,41.1097812328693,
42.084928565179,43.0600758974886,44.0352232297983),.UNSPECIFIED.);
#529=B_SPLINE_CURVE_WITH_KNOTS('',3,(#18340,#18341,#18342,#18343,#18344,
#18345,#18346),.UNSPECIFIED.,.F.,.F.,(4,1,1,1,4),(40.8407044966673,41.7025254316425,
42.6776727639522,43.6528200962618,44.5576896014339),.UNSPECIFIED.);
#530=B_SPLINE_CURVE_WITH_KNOTS('',3,(#18351,#18352,#18353,#18354,#18355,
#18356,#18357,#18358,#18359,#18360),.UNSPECIFIED.,.F.,.F.,(4,1,1,1,1,1,
1,4),(34.5575191894877,35.2588972390113,36.234044571321,37.2091919036307,
38.1843392359403,39.15948656825,40.1346339005596,40.8407044966673),
 .UNSPECIFIED.);
#531=B_SPLINE_CURVE_WITH_KNOTS('',3,(#18361,#18362,#18363,#18364,#18365,
#18366,#18367,#18368,#18369,#18370,#18371),.UNSPECIFIED.,.F.,.F.,(4,1,1,
1,1,1,1,1,4),(34.5575191894877,34.8764941054748,35.8516414377845,36.8267887700942,
37.8019361024038,38.7770834347135,39.7522307670232,40.7273780993328,40.8407044966673),
 .UNSPECIFIED.);
#532=B_SPLINE_CURVE_WITH_KNOTS('',3,(#18376,#18377,#18378,#18379,#18380,
#18381,#18382,#18383,#18384,#18385,#18386),.UNSPECIFIED.,.F.,.F.,(4,1,1,
1,1,1,1,1,4),(28.2743338823081,28.4328659128437,29.4080132451533,30.383160577463,
31.3583079097727,32.3334552420823,33.308602574392,34.2837499067017,34.5575191894877),
 .UNSPECIFIED.);
#533=B_SPLINE_CURVE_WITH_KNOTS('',3,(#18387,#18388,#18389,#18390,#18391,
#18392,#18393,#18394,#18395,#18396),.UNSPECIFIED.,.F.,.F.,(4,1,1,1,1,1,
1,4),(28.2743338823081,29.0256101116168,30.0007574439265,30.9759047762362,
31.9510521085458,32.9261994408555,33.9013467731652,34.5575191894877),
 .UNSPECIFIED.);
#534=B_SPLINE_CURVE_WITH_KNOTS('',3,(#18401,#18402,#18403,#18404,#18405,
#18406,#18407,#18408,#18409,#18410),.UNSPECIFIED.,.F.,.F.,(4,1,1,1,1,1,
1,4),(21.9911485751285,22.5819819189857,23.5571292512954,24.532276583605,
25.5074239159147,26.4825712482243,27.457718580534,28.2743338823081),
 .UNSPECIFIED.);
#535=B_SPLINE_CURVE_WITH_KNOTS('',3,(#18411,#18412,#18413,#18414,#18415,
#18416,#18417,#18418,#18419,#18420,#18421),.UNSPECIFIED.,.F.,.F.,(4,1,1,
1,1,1,1,1,4),(21.9911485751285,22.1995787854492,23.1747261177589,24.1498734500685,
25.1250207823782,26.1001681146879,27.0753154469975,28.0504627793072,28.2743338823081),
 .UNSPECIFIED.);
#536=B_SPLINE_CURVE_WITH_KNOTS('',3,(#18427,#18428,#18429,#18430,#18431),
 .UNSPECIFIED.,.F.,.F.,(4,1,4),(14.3984001269719,15.3735474592815,15.7079632679489),
 .UNSPECIFIED.);
#537=B_SPLINE_CURVE_WITH_KNOTS('',3,(#18434,#18435,#18436,#18437,#18438),
 .UNSPECIFIED.,.F.,.F.,(4,1,4),(13.8759337553363,14.7808032605084,15.7079632679489),
 .UNSPECIFIED.);
#538=B_SPLINE_CURVE_WITH_KNOTS('',3,(#18440,#18441,#18442,#18443,#18444,
#18445,#18446,#18447,#18448,#18449,#18450),.UNSPECIFIED.,.F.,.F.,(4,1,1,
1,1,1,1,1,4),(15.7079632679489,15.755950592818,16.7310979251277,17.7062452574374,
18.681392589747,19.6565399220567,20.6316872543664,21.606834586676,21.9911485751285),
 .UNSPECIFIED.);
#539=B_SPLINE_CURVE_WITH_KNOTS('',3,(#18451,#18452,#18453,#18454,#18455,
#18456,#18457,#18458,#18459,#18460),.UNSPECIFIED.,.F.,.F.,(4,1,1,1,1,1,
1,4),(15.7079632679489,16.3486947915912,17.3238421239009,18.2989894562105,
19.2741367885202,20.2492841208299,21.2244314531395,21.9911485751285),
 .UNSPECIFIED.);
#540=B_SPLINE_CURVE_WITH_KNOTS('',3,(#18605,#18606,#18607,#18608,#18609,
#18610,#18611,#18612,#18613,#18614,#18615,#18616,#18617,#18618,#18619,#18620,
#18621,#18622,#18623,#18624,#18625,#18626,#18627,#18628,#18629,#18630,#18631,
#18632,#18633,#18634,#18635,#18636,#18637,#18638,#18639,#18640,#18641,#18642,
#18643,#18644,#18645,#18646,#18647,#18648,#18649,#18650,#18651,#18652,#18653),
 .UNSPECIFIED.,.F.,.F.,(4,3,3,3,3,3,3,3,3,3,3,3,3,3,3,3,4),(0.,0.0320333804888866,
0.0505515708593653,0.0603413132804416,0.0917900141854983,0.108096115778005,
0.122914675479851,0.145143248337739,0.168151513577436,0.177516949333476,
0.202471322707608,0.21794283081622,0.231200110368267,0.247503117401854,
0.263651632124391,0.277334442830003,0.286347380332244),.UNSPECIFIED.);
#541=B_SPLINE_CURVE_WITH_KNOTS('',3,(#18654,#18655,#18656,#18657,#18658,
#18659,#18660,#18661,#18662,#18663,#18664,#18665,#18666,#18667,#18668,#18669,
#18670,#18671,#18672,#18673,#18674,#18675,#18676,#18677,#18678,#18679,#18680,
#18681,#18682,#18683,#18684,#18685,#18686,#18687,#18688,#18689,#18690,#18691,
#18692,#18693,#18694,#18695,#18696,#18697,#18698,#18699,#18700,#18701,#18702),
 .UNSPECIFIED.,.F.,.F.,(4,3,3,3,3,3,3,3,3,3,3,3,3,3,3,3,4),(0.,0.0274305464075637,
0.0492901149097146,0.0591933555873536,0.0887250095166089,0.100015570674795,
0.108381796308415,0.130826479038955,0.152531076563578,0.162815893631175,
0.190691958353668,0.212372986031639,0.222945305605857,0.245534254906135,
0.257847836118801,0.274320152521146,0.28514280399515),.UNSPECIFIED.);
#542=B_SPLINE_CURVE_WITH_KNOTS('',3,(#18703,#18704,#18705,#18706,#18707,
#18708,#18709,#18710,#18711,#18712,#18713,#18714,#18715,#18716,#18717,#18718,
#18719,#18720,#18721,#18722,#18723,#18724,#18725,#18726,#18727),
 .UNSPECIFIED.,.F.,.F.,(4,3,3,3,3,3,3,3,4),(-10.1357873115492,-9.75147332309665,
-8.77632599078699,-7.80117865847732,-6.82603132616766,-5.85088399385799,
-4.87573666154833,-3.90058932923866,-3.8526020043696),.UNSPECIFIED.);
#543=B_SPLINE_CURVE_WITH_KNOTS('',3,(#18872,#18873,#18874,#18875,#18876,
#18877,#18878,#18879,#18880,#18881,#18882,#18883,#18884,#18885,#18886,#18887,
#18888,#18889,#18890,#18891,#18892,#18893,#18894,#18895,#18896,#18897,#18898,
#18899,#18900,#18901,#18902,#18903,#18904,#18905,#18906,#18907,#18908,#18909,
#18910,#18911,#18912,#18913,#18914,#18915,#18916,#18917,#18918,#18919,#18920),
 .UNSPECIFIED.,.F.,.F.,(4,3,3,3,3,3,3,3,3,3,3,3,3,3,3,3,4),(0.,0.0274305890506951,
0.0492901290331875,0.0591933603491513,0.0887250177779717,0.100015607166709,
0.108381835831352,0.13082647903896,0.152531071764912,0.162815892251191,
0.190691957318683,0.212372984486691,0.22294529735758,0.245534140364172,
0.257847701250626,0.274320152521159,0.285142803995162),.UNSPECIFIED.);
#544=B_SPLINE_CURVE_WITH_KNOTS('',3,(#18921,#18922,#18923,#18924,#18925,
#18926,#18927,#18928,#18929,#18930,#18931,#18932,#18933,#18934,#18935,#18936,
#18937,#18938,#18939,#18940,#18941,#18942,#18943,#18944,#18945),
 .UNSPECIFIED.,.F.,.F.,(4,3,3,3,3,3,3,3,4),(7.59274844815668,7.80117865847732,
8.77632599078698,9.75147332309665,10.7266206554063,11.701767987716,12.6769153200256,
13.6520626523353,13.8759337553363),.UNSPECIFIED.);
#545=B_SPLINE_CURVE_WITH_KNOTS('',3,(#18946,#18947,#18948,#18949,#18950,
#18951,#18952,#18953,#18954,#18955,#18956,#18957,#18958,#18959,#18960,#18961,
#18962,#18963,#18964,#18965,#18966,#18967,#18968,#18969,#18970,#18971,#18972,
#18973,#18974,#18975,#18976,#18977,#18978,#18979,#18980,#18981,#18982,#18983,
#18984,#18985,#18986,#18987,#18988,#18989,#18990,#18991,#18992,#18993,#18994),
 .UNSPECIFIED.,.F.,.F.,(4,3,3,3,3,3,3,3,3,3,3,3,3,3,3,3,4),(0.,0.0320334058164849,
0.0505515938322513,0.0603413311462071,0.0917900214840119,0.108096111687201,
0.122914678304232,0.145143248337743,0.168151527562726,0.177516955081398,
0.202471327018552,0.217942288122009,0.231200024743484,0.24750284136614,
0.263651600306541,0.277334442830014,0.286347380332252),.UNSPECIFIED.);
#554=SHAPE_REPRESENTATION_RELATIONSHIP('SRR','None',#19145,#564);
#564=ADVANCED_BREP_SHAPE_REPRESENTATION('',(#584),#19088);
#574=STYLED_ITEM('',(#19205),#584);
#584=MANIFOLD_SOLID_BREP('Body1',#6828);
#649=FACE_BOUND('',#1640,.T.);
#650=FACE_BOUND('',#1649,.T.);
#803=PLANE('',#7403);
#804=PLANE('',#7405);
#805=PLANE('',#7406);
#806=PLANE('',#7407);
#807=PLANE('',#7408);
#808=PLANE('',#7409);
#809=PLANE('',#7410);
#810=PLANE('',#7411);
#1175=FACE_OUTER_BOUND('',#1626,.T.);
#1176=FACE_OUTER_BOUND('',#1627,.T.);
#1177=FACE_OUTER_BOUND('',#1628,.T.);
#1178=FACE_OUTER_BOUND('',#1629,.T.);
#1179=FACE_OUTER_BOUND('',#1630,.T.);
#1180=FACE_OUTER_BOUND('',#1631,.T.);
#1181=FACE_OUTER_BOUND('',#1632,.T.);
#1182=FACE_OUTER_BOUND('',#1633,.T.);
#1183=FACE_OUTER_BOUND('',#1634,.T.);
#1184=FACE_OUTER_BOUND('',#1635,.T.);
#1185=FACE_OUTER_BOUND('',#1636,.T.);
#1186=FACE_OUTER_BOUND('',#1637,.T.);
#1187=FACE_OUTER_BOUND('',#1638,.T.);
#1188=FACE_OUTER_BOUND('',#1639,.T.);
#1189=FACE_OUTER_BOUND('',#1641,.T.);
#1190=FACE_OUTER_BOUND('',#1642,.T.);
#1191=FACE_OUTER_BOUND('',#1643,.T.);
#1192=FACE_OUTER_BOUND('',#1644,.T.);
#1193=FACE_OUTER_BOUND('',#1645,.T.);
#1194=FACE_OUTER_BOUND('',#1646,.T.);
#1195=FACE_OUTER_BOUND('',#1647,.T.);
#1196=FACE_OUTER_BOUND('',#1648,.T.);
#1626=EDGE_LOOP('',(#6169,#6170,#6171));
#1627=EDGE_LOOP('',(#6172,#6173,#6174,#6175,#6176));
#1628=EDGE_LOOP('',(#6177,#6178,#6179,#6180));
#1629=EDGE_LOOP('',(#6181,#6182,#6183,#6184));
#1630=EDGE_LOOP('',(#6185,#6186,#6187,#6188));
#1631=EDGE_LOOP('',(#6189,#6190,#6191,#6192));
#1632=EDGE_LOOP('',(#6193,#6194,#6195,#6196));
#1633=EDGE_LOOP('',(#6197,#6198,#6199,#6200));
#1634=EDGE_LOOP('',(#6201,#6202,#6203,#6204));
#1635=EDGE_LOOP('',(#6205,#6206,#6207,#6208));
#1636=EDGE_LOOP('',(#6209,#6210,#6211,#6212));
#1637=EDGE_LOOP('',(#6213,#6214,#6215,#6216,#6217,#6218,#6219,#6220,#6221,
#6222,#6223,#6224,#6225,#6226));
#1638=EDGE_LOOP('',(#6227,#6228,#6229,#6230,#6231,#6232,#6233,#6234,#6235,
#6236,#6237,#6238,#6239));
#1639=EDGE_LOOP('',(#6240,#6241,#6242,#6243,#6244,#6245));
#1640=EDGE_LOOP('',(#6246,#6247,#6248,#6249));
#1641=EDGE_LOOP('',(#6250,#6251,#6252,#6253));
#1642=EDGE_LOOP('',(#6254,#6255,#6256,#6257));
#1643=EDGE_LOOP('',(#6258,#6259,#6260,#6261));
#1644=EDGE_LOOP('',(#6262,#6263,#6264,#6265));
#1645=EDGE_LOOP('',(#6266,#6267,#6268,#6269));
#1646=EDGE_LOOP('',(#6270,#6271,#6272,#6273));
#1647=EDGE_LOOP('',(#6274,#6275,#6276,#6277));
#1648=EDGE_LOOP('',(#6278,#6279,#6280,#6281,#6282,#6283));
#1649=EDGE_LOOP('',(#6284,#6285,#6286,#6287,#6288));
#2075=LINE('',#18128,#2524);
#2076=LINE('',#18141,#2525);
#2077=LINE('',#18188,#2526);
#2078=LINE('',#18242,#2527);
#2079=LINE('',#18290,#2528);
#2080=LINE('',#18329,#2529);
#2081=LINE('',#18350,#2530);
#2082=LINE('',#18375,#2531);
#2083=LINE('',#18400,#2532);
#2084=LINE('',#18425,#2533);
#2085=LINE('',#18998,#2534);
#2086=LINE('',#19000,#2535);
#2087=LINE('',#19002,#2536);
#2088=LINE('',#19004,#2537);
#2089=LINE('',#19006,#2538);
#2090=LINE('',#19007,#2539);
#2091=LINE('',#19012,#2540);
#2092=LINE('',#19013,#2541);
#2093=LINE('',#19014,#2542);
#2094=LINE('',#19017,#2543);
#2095=LINE('',#19018,#2544);
#2096=LINE('',#19021,#2545);
#2097=LINE('',#19022,#2546);
#2098=LINE('',#19025,#2547);
#2099=LINE('',#19026,#2548);
#2100=LINE('',#19029,#2549);
#2101=LINE('',#19030,#2550);
#2102=LINE('',#19032,#2551);
#2524=VECTOR('',#8750,0.15);
#2525=VECTOR('',#8755,0.15);
#2526=VECTOR('',#8760,0.15);
#2527=VECTOR('',#8763,0.15);
#2528=VECTOR('',#8766,0.15);
#2529=VECTOR('',#8771,0.1543);
#2530=VECTOR('',#8776,0.1543);
#2531=VECTOR('',#8779,0.1543);
#2532=VECTOR('',#8782,0.1543);
#2533=VECTOR('',#8785,0.1543);
#2534=VECTOR('',#8792,1.);
#2535=VECTOR('',#8793,1.);
#2536=VECTOR('',#8794,1.);
#2537=VECTOR('',#8795,1.);
#2538=VECTOR('',#8796,1.);
#2539=VECTOR('',#8797,1.);
#2540=VECTOR('',#8802,1.);
#2541=VECTOR('',#8803,1.);
#2542=VECTOR('',#8804,1.);
#2543=VECTOR('',#8807,1.);
#2544=VECTOR('',#8808,1.);
#2545=VECTOR('',#8811,1.);
#2546=VECTOR('',#8812,1.);
#2547=VECTOR('',#8815,1.);
#2548=VECTOR('',#8816,1.);
#2549=VECTOR('',#8819,1.);
#2550=VECTOR('',#8820,1.);
#2551=VECTOR('',#8823,1.);
#2705=CIRCLE('',#7388,0.12645);
#2706=CIRCLE('',#7390,0.12645);
#2707=CIRCLE('',#7394,0.12645);
#2708=CIRCLE('',#7396,0.1543);
#2709=CIRCLE('',#7401,0.1543);
#3308=VERTEX_POINT('',#18126);
#3309=VERTEX_POINT('',#18127);
#3310=VERTEX_POINT('',#18129);
#3311=VERTEX_POINT('',#18139);
#3312=VERTEX_POINT('',#18140);
#3313=VERTEX_POINT('',#18142);
#3314=VERTEX_POINT('',#18186);
#3315=VERTEX_POINT('',#18187);
#3316=VERTEX_POINT('',#18240);
#3317=VERTEX_POINT('',#18241);
#3318=VERTEX_POINT('',#18288);
#3319=VERTEX_POINT('',#18289);
#3320=VERTEX_POINT('',#18291);
#3321=VERTEX_POINT('',#18305);
#3322=VERTEX_POINT('',#18327);
#3323=VERTEX_POINT('',#18328);
#3324=VERTEX_POINT('',#18330);
#3325=VERTEX_POINT('',#18338);
#3326=VERTEX_POINT('',#18348);
#3327=VERTEX_POINT('',#18349);
#3328=VERTEX_POINT('',#18373);
#3329=VERTEX_POINT('',#18374);
#3330=VERTEX_POINT('',#18398);
#3331=VERTEX_POINT('',#18399);
#3332=VERTEX_POINT('',#18423);
#3333=VERTEX_POINT('',#18424);
#3334=VERTEX_POINT('',#18426);
#3335=VERTEX_POINT('',#18432);
#3336=VERTEX_POINT('',#18996);
#3337=VERTEX_POINT('',#18997);
#3338=VERTEX_POINT('',#18999);
#3339=VERTEX_POINT('',#19001);
#3340=VERTEX_POINT('',#19003);
#3341=VERTEX_POINT('',#19005);
#3342=VERTEX_POINT('',#19010);
#3343=VERTEX_POINT('',#19011);
#3344=VERTEX_POINT('',#19016);
#3345=VERTEX_POINT('',#19020);
#3346=VERTEX_POINT('',#19024);
#3347=VERTEX_POINT('',#19028);
#4269=EDGE_CURVE('',#3308,#3309,#2075,.T.);
#4270=EDGE_CURVE('',#3310,#3309,#2705,.F.);
#4271=EDGE_CURVE('',#3310,#3308,#519,.T.);
#4272=EDGE_CURVE('',#3311,#3312,#2076,.T.);
#4273=EDGE_CURVE('',#3312,#3313,#520,.T.);
#4274=EDGE_CURVE('',#3309,#3313,#2706,.F.);
#4275=EDGE_CURVE('',#3308,#3311,#521,.T.);
#4276=EDGE_CURVE('',#3314,#3315,#2077,.T.);
#4277=EDGE_CURVE('',#3315,#3312,#522,.T.);
#4278=EDGE_CURVE('',#3311,#3314,#523,.T.);
#4279=EDGE_CURVE('',#3316,#3317,#2078,.T.);
#4280=EDGE_CURVE('',#3317,#3315,#524,.T.);
#4281=EDGE_CURVE('',#3314,#3316,#525,.T.);
#4282=EDGE_CURVE('',#3318,#3319,#2079,.T.);
#4283=EDGE_CURVE('',#3318,#3320,#526,.T.);
#4284=EDGE_CURVE('',#3321,#3320,#2707,.T.);
#4285=EDGE_CURVE('',#3321,#3319,#527,.T.);
#4286=EDGE_CURVE('',#3322,#3323,#2080,.T.);
#4287=EDGE_CURVE('',#3323,#3324,#528,.T.);
#4288=EDGE_CURVE('',#3325,#3324,#2708,.T.);
#4289=EDGE_CURVE('',#3322,#3325,#529,.T.);
#4290=EDGE_CURVE('',#3326,#3327,#2081,.T.);
#4291=EDGE_CURVE('',#3327,#3323,#530,.T.);
#4292=EDGE_CURVE('',#3326,#3322,#531,.T.);
#4293=EDGE_CURVE('',#3328,#3329,#2082,.T.);
#4294=EDGE_CURVE('',#3329,#3327,#532,.T.);
#4295=EDGE_CURVE('',#3328,#3326,#533,.T.);
#4296=EDGE_CURVE('',#3330,#3331,#2083,.T.);
#4297=EDGE_CURVE('',#3331,#3329,#534,.T.);
#4298=EDGE_CURVE('',#3330,#3328,#535,.T.);
#4299=EDGE_CURVE('',#3332,#3333,#2084,.T.);
#4300=EDGE_CURVE('',#3334,#3332,#536,.T.);
#4301=EDGE_CURVE('',#3335,#3334,#2709,.T.);
#4302=EDGE_CURVE('',#3335,#3333,#537,.T.);
#4303=EDGE_CURVE('',#3333,#3331,#538,.T.);
#4304=EDGE_CURVE('',#3332,#3330,#539,.T.);
#4305=EDGE_CURVE('',#3324,#3310,#540,.T.);
#4306=EDGE_CURVE('',#3320,#3335,#541,.T.);
#4307=EDGE_CURVE('',#3316,#3318,#542,.T.);
#4308=EDGE_CURVE('',#3313,#3325,#543,.T.);
#4309=EDGE_CURVE('',#3319,#3317,#544,.T.);
#4310=EDGE_CURVE('',#3334,#3321,#545,.T.);
#4311=EDGE_CURVE('',#3336,#3337,#2085,.T.);
#4312=EDGE_CURVE('',#3337,#3338,#2086,.T.);
#4313=EDGE_CURVE('',#3338,#3339,#2087,.T.);
#4314=EDGE_CURVE('',#3339,#3340,#2088,.T.);
#4315=EDGE_CURVE('',#3340,#3341,#2089,.T.);
#4316=EDGE_CURVE('',#3341,#3336,#2090,.T.);
#4317=EDGE_CURVE('',#3342,#3343,#2091,.T.);
#4318=EDGE_CURVE('',#3343,#3336,#2092,.T.);
#4319=EDGE_CURVE('',#3342,#3341,#2093,.T.);
#4320=EDGE_CURVE('',#3344,#3342,#2094,.T.);
#4321=EDGE_CURVE('',#3344,#3340,#2095,.T.);
#4322=EDGE_CURVE('',#3345,#3344,#2096,.T.);
#4323=EDGE_CURVE('',#3345,#3339,#2097,.T.);
#4324=EDGE_CURVE('',#3346,#3345,#2098,.T.);
#4325=EDGE_CURVE('',#3346,#3338,#2099,.T.);
#4326=EDGE_CURVE('',#3347,#3346,#2100,.T.);
#4327=EDGE_CURVE('',#3347,#3337,#2101,.T.);
#4328=EDGE_CURVE('',#3343,#3347,#2102,.T.);
#6169=ORIENTED_EDGE('',*,*,#4269,.T.);
#6170=ORIENTED_EDGE('',*,*,#4270,.F.);
#6171=ORIENTED_EDGE('',*,*,#4271,.T.);
#6172=ORIENTED_EDGE('',*,*,#4272,.T.);
#6173=ORIENTED_EDGE('',*,*,#4273,.T.);
#6174=ORIENTED_EDGE('',*,*,#4274,.F.);
#6175=ORIENTED_EDGE('',*,*,#4269,.F.);
#6176=ORIENTED_EDGE('',*,*,#4275,.T.);
#6177=ORIENTED_EDGE('',*,*,#4276,.T.);
#6178=ORIENTED_EDGE('',*,*,#4277,.T.);
#6179=ORIENTED_EDGE('',*,*,#4272,.F.);
#6180=ORIENTED_EDGE('',*,*,#4278,.T.);
#6181=ORIENTED_EDGE('',*,*,#4279,.T.);
#6182=ORIENTED_EDGE('',*,*,#4280,.T.);
#6183=ORIENTED_EDGE('',*,*,#4276,.F.);
#6184=ORIENTED_EDGE('',*,*,#4281,.T.);
#6185=ORIENTED_EDGE('',*,*,#4282,.F.);
#6186=ORIENTED_EDGE('',*,*,#4283,.T.);
#6187=ORIENTED_EDGE('',*,*,#4284,.F.);
#6188=ORIENTED_EDGE('',*,*,#4285,.T.);
#6189=ORIENTED_EDGE('',*,*,#4286,.T.);
#6190=ORIENTED_EDGE('',*,*,#4287,.T.);
#6191=ORIENTED_EDGE('',*,*,#4288,.F.);
#6192=ORIENTED_EDGE('',*,*,#4289,.F.);
#6193=ORIENTED_EDGE('',*,*,#4290,.T.);
#6194=ORIENTED_EDGE('',*,*,#4291,.T.);
#6195=ORIENTED_EDGE('',*,*,#4286,.F.);
#6196=ORIENTED_EDGE('',*,*,#4292,.F.);
#6197=ORIENTED_EDGE('',*,*,#4293,.T.);
#6198=ORIENTED_EDGE('',*,*,#4294,.T.);
#6199=ORIENTED_EDGE('',*,*,#4290,.F.);
#6200=ORIENTED_EDGE('',*,*,#4295,.F.);
#6201=ORIENTED_EDGE('',*,*,#4296,.T.);
#6202=ORIENTED_EDGE('',*,*,#4297,.T.);
#6203=ORIENTED_EDGE('',*,*,#4293,.F.);
#6204=ORIENTED_EDGE('',*,*,#4298,.F.);
#6205=ORIENTED_EDGE('',*,*,#4299,.F.);
#6206=ORIENTED_EDGE('',*,*,#4300,.F.);
#6207=ORIENTED_EDGE('',*,*,#4301,.F.);
#6208=ORIENTED_EDGE('',*,*,#4302,.T.);
#6209=ORIENTED_EDGE('',*,*,#4299,.T.);
#6210=ORIENTED_EDGE('',*,*,#4303,.T.);
#6211=ORIENTED_EDGE('',*,*,#4296,.F.);
#6212=ORIENTED_EDGE('',*,*,#4304,.F.);
#6213=ORIENTED_EDGE('',*,*,#4305,.F.);
#6214=ORIENTED_EDGE('',*,*,#4287,.F.);
#6215=ORIENTED_EDGE('',*,*,#4291,.F.);
#6216=ORIENTED_EDGE('',*,*,#4294,.F.);
#6217=ORIENTED_EDGE('',*,*,#4297,.F.);
#6218=ORIENTED_EDGE('',*,*,#4303,.F.);
#6219=ORIENTED_EDGE('',*,*,#4302,.F.);
#6220=ORIENTED_EDGE('',*,*,#4306,.F.);
#6221=ORIENTED_EDGE('',*,*,#4283,.F.);
#6222=ORIENTED_EDGE('',*,*,#4307,.F.);
#6223=ORIENTED_EDGE('',*,*,#4281,.F.);
#6224=ORIENTED_EDGE('',*,*,#4278,.F.);
#6225=ORIENTED_EDGE('',*,*,#4275,.F.);
#6226=ORIENTED_EDGE('',*,*,#4271,.F.);
#6227=ORIENTED_EDGE('',*,*,#4308,.F.);
#6228=ORIENTED_EDGE('',*,*,#4273,.F.);
#6229=ORIENTED_EDGE('',*,*,#4277,.F.);
#6230=ORIENTED_EDGE('',*,*,#4280,.F.);
#6231=ORIENTED_EDGE('',*,*,#4309,.F.);
#6232=ORIENTED_EDGE('',*,*,#4285,.F.);
#6233=ORIENTED_EDGE('',*,*,#4310,.F.);
#6234=ORIENTED_EDGE('',*,*,#4300,.T.);
#6235=ORIENTED_EDGE('',*,*,#4304,.T.);
#6236=ORIENTED_EDGE('',*,*,#4298,.T.);
#6237=ORIENTED_EDGE('',*,*,#4295,.T.);
#6238=ORIENTED_EDGE('',*,*,#4292,.T.);
#6239=ORIENTED_EDGE('',*,*,#4289,.T.);
#6240=ORIENTED_EDGE('',*,*,#4311,.T.);
#6241=ORIENTED_EDGE('',*,*,#4312,.T.);
#6242=ORIENTED_EDGE('',*,*,#4313,.T.);
#6243=ORIENTED_EDGE('',*,*,#4314,.T.);
#6244=ORIENTED_EDGE('',*,*,#4315,.T.);
#6245=ORIENTED_EDGE('',*,*,#4316,.T.);
#6246=ORIENTED_EDGE('',*,*,#4306,.T.);
#6247=ORIENTED_EDGE('',*,*,#4301,.T.);
#6248=ORIENTED_EDGE('',*,*,#4310,.T.);
#6249=ORIENTED_EDGE('',*,*,#4284,.T.);
#6250=ORIENTED_EDGE('',*,*,#4282,.T.);
#6251=ORIENTED_EDGE('',*,*,#4309,.T.);
#6252=ORIENTED_EDGE('',*,*,#4279,.F.);
#6253=ORIENTED_EDGE('',*,*,#4307,.T.);
#6254=ORIENTED_EDGE('',*,*,#4317,.T.);
#6255=ORIENTED_EDGE('',*,*,#4318,.T.);
#6256=ORIENTED_EDGE('',*,*,#4316,.F.);
#6257=ORIENTED_EDGE('',*,*,#4319,.F.);
#6258=ORIENTED_EDGE('',*,*,#4320,.T.);
#6259=ORIENTED_EDGE('',*,*,#4319,.T.);
#6260=ORIENTED_EDGE('',*,*,#4315,.F.);
#6261=ORIENTED_EDGE('',*,*,#4321,.F.);
#6262=ORIENTED_EDGE('',*,*,#4322,.T.);
#6263=ORIENTED_EDGE('',*,*,#4321,.T.);
#6264=ORIENTED_EDGE('',*,*,#4314,.F.);
#6265=ORIENTED_EDGE('',*,*,#4323,.F.);
#6266=ORIENTED_EDGE('',*,*,#4324,.T.);
#6267=ORIENTED_EDGE('',*,*,#4323,.T.);
#6268=ORIENTED_EDGE('',*,*,#4313,.F.);
#6269=ORIENTED_EDGE('',*,*,#4325,.F.);
#6270=ORIENTED_EDGE('',*,*,#4326,.T.);
#6271=ORIENTED_EDGE('',*,*,#4325,.T.);
#6272=ORIENTED_EDGE('',*,*,#4312,.F.);
#6273=ORIENTED_EDGE('',*,*,#4327,.F.);
#6274=ORIENTED_EDGE('',*,*,#4328,.T.);
#6275=ORIENTED_EDGE('',*,*,#4327,.T.);
#6276=ORIENTED_EDGE('',*,*,#4311,.F.);
#6277=ORIENTED_EDGE('',*,*,#4318,.F.);
#6278=ORIENTED_EDGE('',*,*,#4328,.F.);
#6279=ORIENTED_EDGE('',*,*,#4317,.F.);
#6280=ORIENTED_EDGE('',*,*,#4320,.F.);
#6281=ORIENTED_EDGE('',*,*,#4322,.F.);
#6282=ORIENTED_EDGE('',*,*,#4324,.F.);
#6283=ORIENTED_EDGE('',*,*,#4326,.F.);
#6284=ORIENTED_EDGE('',*,*,#4305,.T.);
#6285=ORIENTED_EDGE('',*,*,#4270,.T.);
#6286=ORIENTED_EDGE('',*,*,#4274,.T.);
#6287=ORIENTED_EDGE('',*,*,#4308,.T.);
#6288=ORIENTED_EDGE('',*,*,#4288,.T.);
#6418=CYLINDRICAL_SURFACE('',#7387,0.12645);
#6419=CYLINDRICAL_SURFACE('',#7389,0.12645);
#6420=CYLINDRICAL_SURFACE('',#7391,0.12645);
#6421=CYLINDRICAL_SURFACE('',#7392,0.12645);
#6422=CYLINDRICAL_SURFACE('',#7393,0.12645);
#6423=CYLINDRICAL_SURFACE('',#7395,0.1543);
#6424=CYLINDRICAL_SURFACE('',#7397,0.1543);
#6425=CYLINDRICAL_SURFACE('',#7398,0.1543);
#6426=CYLINDRICAL_SURFACE('',#7399,0.1543);
#6427=CYLINDRICAL_SURFACE('',#7400,0.1543);
#6428=CYLINDRICAL_SURFACE('',#7402,0.1543);
#6429=CYLINDRICAL_SURFACE('',#7404,0.12645);
#6794=ADVANCED_FACE('',(#1175),#6418,.F.);
#6795=ADVANCED_FACE('',(#1176),#6419,.F.);
#6796=ADVANCED_FACE('',(#1177),#6420,.F.);
#6797=ADVANCED_FACE('',(#1178),#6421,.F.);
#6798=ADVANCED_FACE('',(#1179),#6422,.F.);
#6799=ADVANCED_FACE('',(#1180),#6423,.F.);
#6800=ADVANCED_FACE('',(#1181),#6424,.F.);
#6801=ADVANCED_FACE('',(#1182),#6425,.F.);
#6802=ADVANCED_FACE('',(#1183),#6426,.F.);
#6803=ADVANCED_FACE('',(#1184),#6427,.F.);
#6804=ADVANCED_FACE('',(#1185),#6428,.F.);
#6805=ADVANCED_FACE('',(#1186),#170,.F.);
#6806=ADVANCED_FACE('',(#1187),#171,.F.);
#6807=ADVANCED_FACE('',(#1188,#649),#803,.T.);
#6808=ADVANCED_FACE('',(#1189),#6429,.F.);
#6809=ADVANCED_FACE('',(#1190),#804,.T.);
#6810=ADVANCED_FACE('',(#1191),#805,.T.);
#6811=ADVANCED_FACE('',(#1192),#806,.T.);
#6812=ADVANCED_FACE('',(#1193),#807,.T.);
#6813=ADVANCED_FACE('',(#1194),#808,.T.);
#6814=ADVANCED_FACE('',(#1195),#809,.T.);
#6815=ADVANCED_FACE('',(#1196,#650),#810,.F.);
#6828=CLOSED_SHELL('',(#6794,#6795,#6796,#6797,#6798,#6799,#6800,#6801,
#6802,#6803,#6804,#6805,#6806,#6807,#6808,#6809,#6810,#6811,#6812,#6813,
#6814,#6815));
#7386=AXIS2_PLACEMENT_3D('',#18124,#8746,#8747);
#7387=AXIS2_PLACEMENT_3D('',#18125,#8748,#8749);
#7388=AXIS2_PLACEMENT_3D('',#18130,#8751,#8752);
#7389=AXIS2_PLACEMENT_3D('',#18138,#8753,#8754);
#7390=AXIS2_PLACEMENT_3D('',#18162,#8756,#8757);
#7391=AXIS2_PLACEMENT_3D('',#18185,#8758,#8759);
#7392=AXIS2_PLACEMENT_3D('',#18239,#8761,#8762);
#7393=AXIS2_PLACEMENT_3D('',#18287,#8764,#8765);
#7394=AXIS2_PLACEMENT_3D('',#18306,#8767,#8768);
#7395=AXIS2_PLACEMENT_3D('',#18326,#8769,#8770);
#7396=AXIS2_PLACEMENT_3D('',#18339,#8772,#8773);
#7397=AXIS2_PLACEMENT_3D('',#18347,#8774,#8775);
#7398=AXIS2_PLACEMENT_3D('',#18372,#8777,#8778);
#7399=AXIS2_PLACEMENT_3D('',#18397,#8780,#8781);
#7400=AXIS2_PLACEMENT_3D('',#18422,#8783,#8784);
#7401=AXIS2_PLACEMENT_3D('',#18433,#8786,#8787);
#7402=AXIS2_PLACEMENT_3D('',#18439,#8788,#8789);
#7403=AXIS2_PLACEMENT_3D('',#18995,#8790,#8791);
#7404=AXIS2_PLACEMENT_3D('',#19008,#8798,#8799);
#7405=AXIS2_PLACEMENT_3D('',#19009,#8800,#8801);
#7406=AXIS2_PLACEMENT_3D('',#19015,#8805,#8806);
#7407=AXIS2_PLACEMENT_3D('',#19019,#8809,#8810);
#7408=AXIS2_PLACEMENT_3D('',#19023,#8813,#8814);
#7409=AXIS2_PLACEMENT_3D('',#19027,#8817,#8818);
#7410=AXIS2_PLACEMENT_3D('',#19031,#8821,#8822);
#7411=AXIS2_PLACEMENT_3D('',#19033,#8824,#8825);
#8746=DIRECTION('axis',(0.,0.,1.));
#8747=DIRECTION('refdir',(1.,0.,0.));
#8748=DIRECTION('center_axis',(0.,0.,-1.));
#8749=DIRECTION('ref_axis',(1.,0.,0.));
#8750=DIRECTION('',(0.,0.,-1.));
#8751=DIRECTION('center_axis',(0.,0.,-1.));
#8752=DIRECTION('ref_axis',(1.,0.,0.));
#8753=DIRECTION('center_axis',(0.,0.,-1.));
#8754=DIRECTION('ref_axis',(1.,0.,0.));
#8755=DIRECTION('',(0.,0.,-1.));
#8756=DIRECTION('center_axis',(0.,0.,-1.));
#8757=DIRECTION('ref_axis',(1.,0.,0.));
#8758=DIRECTION('center_axis',(0.,0.,-1.));
#8759=DIRECTION('ref_axis',(1.,0.,0.));
#8760=DIRECTION('',(0.,0.,-1.));
#8761=DIRECTION('center_axis',(0.,0.,-1.));
#8762=DIRECTION('ref_axis',(1.,0.,0.));
#8763=DIRECTION('',(0.,0.,-1.));
#8764=DIRECTION('center_axis',(0.,0.,-1.));
#8765=DIRECTION('ref_axis',(0.937385399639056,-0.348293859468591,0.));
#8766=DIRECTION('',(0.,0.,-1.));
#8767=DIRECTION('center_axis',(0.,0.,-1.));
#8768=DIRECTION('ref_axis',(1.,0.,0.));
#8769=DIRECTION('center_axis',(0.,0.,-1.));
#8770=DIRECTION('ref_axis',(0.28361887368566,0.958937085782627,0.));
#8771=DIRECTION('',(1.22464679914735E-16,8.07419868282478E-31,-1.));
#8772=DIRECTION('center_axis',(0.,0.,1.));
#8773=DIRECTION('ref_axis',(1.,6.71554824363804E-15,0.));
#8774=DIRECTION('center_axis',(0.,0.,-1.));
#8775=DIRECTION('ref_axis',(1.,6.71554824363804E-15,0.));
#8776=DIRECTION('',(1.22464679914735E-16,8.07419868282478E-31,-1.));
#8777=DIRECTION('center_axis',(0.,0.,-1.));
#8778=DIRECTION('ref_axis',(1.,6.71554824363804E-15,0.));
#8779=DIRECTION('',(1.22464679914735E-16,8.07419868282478E-31,-1.));
#8780=DIRECTION('center_axis',(0.,0.,-1.));
#8781=DIRECTION('ref_axis',(1.,6.71554824363804E-15,0.));
#8782=DIRECTION('',(1.22464679914735E-16,8.07419868282478E-31,-1.));
#8783=DIRECTION('center_axis',(0.,0.,-1.));
#8784=DIRECTION('ref_axis',(-0.60895050335979,-0.793208222636313,0.));
#8785=DIRECTION('',(1.22464679914735E-16,8.07419868282478E-31,-1.));
#8786=DIRECTION('center_axis',(0.,0.,-1.));
#8787=DIRECTION('ref_axis',(1.,6.71554824363804E-15,0.));
#8788=DIRECTION('center_axis',(0.,0.,-1.));
#8789=DIRECTION('ref_axis',(1.,6.71554824363804E-15,0.));
#8790=DIRECTION('center_axis',(0.,0.,1.));
#8791=DIRECTION('ref_axis',(1.,0.,0.));
#8792=DIRECTION('',(0.5,0.866025403784439,0.));
#8793=DIRECTION('',(-0.5,0.866025403784439,0.));
#8794=DIRECTION('',(-1.,0.,0.));
#8795=DIRECTION('',(-0.5,-0.866025403784439,0.));
#8796=DIRECTION('',(0.5,-0.866025403784439,0.));
#8797=DIRECTION('',(1.,-3.49629579342466E-16,0.));
#8798=DIRECTION('center_axis',(0.,0.,-1.));
#8799=DIRECTION('ref_axis',(1.,0.,0.));
#8800=DIRECTION('center_axis',(-3.49629579342466E-16,-1.,0.));
#8801=DIRECTION('ref_axis',(1.,-3.49629579342466E-16,0.));
#8802=DIRECTION('',(1.,-3.49629579342466E-16,0.));
#8803=DIRECTION('',(0.,0.,1.));
#8804=DIRECTION('',(0.,0.,1.));
#8805=DIRECTION('center_axis',(-0.866025403784439,-0.5,0.));
#8806=DIRECTION('ref_axis',(0.5,-0.866025403784439,0.));
#8807=DIRECTION('',(0.5,-0.866025403784439,0.));
#8808=DIRECTION('',(0.,0.,1.));
#8809=DIRECTION('center_axis',(-0.866025403784439,0.5,0.));
#8810=DIRECTION('ref_axis',(-0.5,-0.866025403784439,0.));
#8811=DIRECTION('',(-0.5,-0.866025403784439,0.));
#8812=DIRECTION('',(0.,0.,1.));
#8813=DIRECTION('center_axis',(0.,1.,0.));
#8814=DIRECTION('ref_axis',(-1.,0.,0.));
#8815=DIRECTION('',(-1.,0.,0.));
#8816=DIRECTION('',(0.,0.,1.));
#8817=DIRECTION('center_axis',(0.866025403784439,0.5,0.));
#8818=DIRECTION('ref_axis',(-0.5,0.866025403784439,0.));
#8819=DIRECTION('',(-0.5,0.866025403784439,0.));
#8820=DIRECTION('',(0.,0.,1.));
#8821=DIRECTION('center_axis',(0.866025403784439,-0.5,0.));
#8822=DIRECTION('ref_axis',(0.5,0.866025403784439,0.));
#8823=DIRECTION('',(0.5,0.866025403784439,0.));
#8824=DIRECTION('center_axis',(0.,0.,1.));
#8825=DIRECTION('ref_axis',(1.,0.,0.));
#18124=CARTESIAN_POINT('',(0.,0.,0.));
#18125=CARTESIAN_POINT('Origin',(0.,0.,0.12));
#18126=CARTESIAN_POINT('',(-0.12639138516214,8.91322620741042E-5,0.00934196736194174));
#18127=CARTESIAN_POINT('',(-0.12645,1.54856587752183E-17,-5.55111512312578E-17));
#18128=CARTESIAN_POINT('',(-0.12645,1.54856587752183E-17,0.12));
#18129=CARTESIAN_POINT('',(-0.0488748409397564,0.116622692573588,0.));
#18130=CARTESIAN_POINT('Origin',(0.,0.,0.));
#18131=CARTESIAN_POINT('Ctrl Pts',(-0.0489111879062984,0.116810626195002,
1.20007714660797E-17));
#18132=CARTESIAN_POINT('Ctrl Pts',(-0.0838963038512042,0.101957324585112,
0.00240024091002088));
#18133=CARTESIAN_POINT('Ctrl Pts',(-0.11198221847721,0.0702793053867637,
0.00480048182004174));
#18134=CARTESIAN_POINT('Ctrl Pts',(-0.122072221370749,0.0336561163696377,
0.00720072273006261));
#18135=CARTESIAN_POINT('Ctrl Pts',(-0.125072637487486,0.022765653033531,
0.00791447094068899));
#18136=CARTESIAN_POINT('Ctrl Pts',(-0.126481745582665,0.0114379076904012,
0.00862821915131536));
#18137=CARTESIAN_POINT('Ctrl Pts',(-0.12639138516214,8.91322620741042E-5,
0.00934196736194174));
#18138=CARTESIAN_POINT('Origin',(0.,0.,0.12));
#18139=CARTESIAN_POINT('',(-0.126396145829628,-9.95859796292312E-5,0.0593419673619417));
#18140=CARTESIAN_POINT('',(-0.126575671592806,-7.20628672610732E-5,0.0456580326380584));
#18141=CARTESIAN_POINT('',(-0.12645,1.54856587752183E-17,0.12));
#18142=CARTESIAN_POINT('',(-0.10808967569503,-0.0656218295092665,0.));
#18143=CARTESIAN_POINT('Ctrl Pts',(-0.126575671592806,-7.20628672610732E-5,
0.0456580326380584));
#18144=CARTESIAN_POINT('Ctrl Pts',(-0.126327459688109,0.0361497101693465,
0.0433719816070355));
#18145=CARTESIAN_POINT('Ctrl Pts',(-0.109912066394173,0.0725710138228805,
0.0410859305760125));
#18146=CARTESIAN_POINT('Ctrl Pts',(-0.0824515099939393,0.0961223418729112,
0.0387998795449896));
#18147=CARTESIAN_POINT('Ctrl Pts',(-0.05137998778939,0.122770586059505,
0.036213220908657));
#18148=CARTESIAN_POINT('Ctrl Pts',(-0.00616751748104999,0.132941603485868,
0.0336265622723243));
#18149=CARTESIAN_POINT('Ctrl Pts',(0.0333172074018229,0.122176268745047,
0.0310399036359917));
#18150=CARTESIAN_POINT('Ctrl Pts',(0.0728019322846963,0.111410934004226,
0.028453244999659));
#18151=CARTESIAN_POINT('Ctrl Pts',(0.106558911742102,0.0797092470962188,
0.0258665863633264));
#18152=CARTESIAN_POINT('Ctrl Pts',(0.11981357554495,0.0409763259700822,
0.0232799277269937));
#18153=CARTESIAN_POINT('Ctrl Pts',(0.133068239347797,0.00224340484394604,
0.0206932690906611));
#18154=CARTESIAN_POINT('Ctrl Pts',(0.125820587496086,-0.0435207505003201,
0.0181066104543285));
#18155=CARTESIAN_POINT('Ctrl Pts',(0.101166903546451,-0.0762076816581678,
0.0155199518179958));
#18156=CARTESIAN_POINT('Ctrl Pts',(0.0765132195968157,-0.108894612816016,
0.0129332931816632));
#18157=CARTESIAN_POINT('Ctrl Pts',(0.0344535035492562,-0.128504319787445,
0.0103466345453306));
#18158=CARTESIAN_POINT('Ctrl Pts',(-0.00636464094143544,-0.126469737202777,
0.00775997590899791));
#18159=CARTESIAN_POINT('Ctrl Pts',(-0.0471827854321269,-0.124435154618108,
0.00517331727266527));
#18160=CARTESIAN_POINT('Ctrl Pts',(-0.0867593583659505,-0.100756282477341,
0.00258665863633259));
#18161=CARTESIAN_POINT('Ctrl Pts',(-0.108089675695031,-0.0656218295092657,
-5.55111512312578E-17));
#18162=CARTESIAN_POINT('Origin',(0.,0.,0.));
#18163=CARTESIAN_POINT('Ctrl Pts',(-0.12639138516214,8.91322620741042E-5,
0.00934196736194174));
#18164=CARTESIAN_POINT('Ctrl Pts',(-0.126154274972366,-0.0296906128949183,
0.011214877787648));
#18165=CARTESIAN_POINT('Ctrl Pts',(-0.115592373032178,-0.0596151635265703,
0.0130877882133543));
#18166=CARTESIAN_POINT('Ctrl Pts',(-0.0963650578556872,-0.0821635787359664,
0.0149606986390606));
#18167=CARTESIAN_POINT('Ctrl Pts',(-0.0698103971670931,-0.113304978845907,
0.0175473572753932));
#18168=CARTESIAN_POINT('Ctrl Pts',(-0.0267272342632827,-0.130377059081323,
0.0201340159117258));
#18169=CARTESIAN_POINT('Ctrl Pts',(0.0139574509341311,-0.125868770046104,
0.0227206745480584));
#18170=CARTESIAN_POINT('Ctrl Pts',(0.0546421361315456,-0.121360481010885,
0.0253073331843911));
#18171=CARTESIAN_POINT('Ctrl Pts',(0.0929283436225635,-0.0952718227050311,
0.0278939918207237));
#18172=CARTESIAN_POINT('Ctrl Pts',(0.112018291148455,-0.0590635258734944,
0.0304806504570564));
#18173=CARTESIAN_POINT('Ctrl Pts',(0.131108238674346,-0.0228552290419586,
0.033067309093389));
#18174=CARTESIAN_POINT('Ctrl Pts',(0.131001926235112,0.0234727063152593,
0.0356539677297216));
#18175=CARTESIAN_POINT('Ctrl Pts',(0.111741771403992,0.0595891814911641,
0.0382406263660542));
#18176=CARTESIAN_POINT('Ctrl Pts',(0.0924816165728724,0.0957056566670696,
0.0408272850023869));
#18177=CARTESIAN_POINT('Ctrl Pts',(0.0540676193498672,0.121610671661662,
0.0434139436387195));
#18178=CARTESIAN_POINT('Ctrl Pts',(0.0133639835211523,0.125930636937597,
0.0460006022750522));
#18179=CARTESIAN_POINT('Ctrl Pts',(-0.0273396523075625,0.130250602213533,
0.0485872609113848));
#18180=CARTESIAN_POINT('Ctrl Pts',(-0.0703329267419868,0.112985517770812,
0.0511739195477175));
#18181=CARTESIAN_POINT('Ctrl Pts',(-0.0967449447385466,0.0817152626609385,
0.0537605781840501));
#18182=CARTESIAN_POINT('Ctrl Pts',(-0.115741878896724,0.0592240248649833,
0.0556210412433473));
#18183=CARTESIAN_POINT('Ctrl Pts',(-0.126160906676814,0.0294875554882879,
0.0574815043026445));
#18184=CARTESIAN_POINT('Ctrl Pts',(-0.126396145829628,-9.95859796292312E-5,
0.0593419673619417));
#18185=CARTESIAN_POINT('Origin',(0.,0.,0.12));
#18186=CARTESIAN_POINT('',(-0.126529791093031,9.025049583615E-5,0.109341967361942));
#18187=CARTESIAN_POINT('',(-0.126349242904067,8.85860673823967E-5,0.0956580326380584));
#18188=CARTESIAN_POINT('',(-0.12645,1.54856587752183E-17,0.12));
#18189=CARTESIAN_POINT('Ctrl Pts',(-0.126349242904067,8.85860673823967E-5,
0.0956580326380584));
#18190=CARTESIAN_POINT('Ctrl Pts',(-0.126441591528965,0.0135570965972842,
0.0948119253946973));
#18191=CARTESIAN_POINT('Ctrl Pts',(-0.124448136217638,0.0269990101701626,
0.0939658181513361));
#18192=CARTESIAN_POINT('Ctrl Pts',(-0.120249444863787,0.0397126388809939,
0.093119710907975));
#18193=CARTESIAN_POINT('Ctrl Pts',(-0.107413505522824,0.0785798365820317,
0.0905330522716423));
#18194=CARTESIAN_POINT('Ctrl Pts',(-0.0739673525896496,0.110640458354997,
0.0879463936353097));
#18195=CARTESIAN_POINT('Ctrl Pts',(-0.0345920580258737,0.121821308595361,
0.085359734998977));
#18196=CARTESIAN_POINT('Ctrl Pts',(0.00478323653790218,0.133002158835724,
0.0827730763626444));
#18197=CARTESIAN_POINT('Ctrl Pts',(0.0500876727322792,0.123303237543486,
0.0801864177263117));
#18198=CARTESIAN_POINT('Ctrl Pts',(0.0814342209129887,0.0969820390626645,
0.077599759089979));
#18199=CARTESIAN_POINT('Ctrl Pts',(0.112780769093698,0.0706608405818426,
0.0750131004536464));
#18200=CARTESIAN_POINT('Ctrl Pts',(0.13016942926074,0.0277173649124373,
0.0724264418173139));
#18201=CARTESIAN_POINT('Ctrl Pts',(0.12596827751407,-0.0129984006283456,
0.0698397831809812));
#18202=CARTESIAN_POINT('Ctrl Pts',(0.121767125767399,-0.0537141661691284,
0.0672531245446486));
#18203=CARTESIAN_POINT('Ctrl Pts',(0.0959761621070158,-0.0922022215812886,
0.0646664659083159));
#18204=CARTESIAN_POINT('Ctrl Pts',(0.059914723710966,-0.111567668284471,
0.0620798072719833));
#18205=CARTESIAN_POINT('Ctrl Pts',(0.0238532853149157,-0.130933114987654,
0.0594931486356506));
#18206=CARTESIAN_POINT('Ctrl Pts',(-0.0224786278168013,-0.131175952981858,
0.056906489999318));
#18207=CARTESIAN_POINT('Ctrl Pts',(-0.0587401909579078,-0.112190380850839,
0.0543198313629853));
#18208=CARTESIAN_POINT('Ctrl Pts',(-0.0950017540990138,-0.0932048087198191,
0.0517331727266527));
#18209=CARTESIAN_POINT('Ctrl Pts',(-0.12119296724951,-0.0549908264635757,
0.0491465140903201));
#18210=CARTESIAN_POINT('Ctrl Pts',(-0.125823286774378,-0.0143210998620416,
0.0465598554539874));
#18211=CARTESIAN_POINT('Ctrl Pts',(-0.126361397696569,-0.0095946821776348,
0.0462592478486778));
#18212=CARTESIAN_POINT('Ctrl Pts',(-0.12660831057823,-0.00483509759607578,
0.0459586402433681));
#18213=CARTESIAN_POINT('Ctrl Pts',(-0.126575671592806,-7.20628672610732E-5,
0.0456580326380584));
#18214=CARTESIAN_POINT('Ctrl Pts',(-0.126396145829628,-9.95859796292312E-5,
0.0593419673619417));
#18215=CARTESIAN_POINT('Ctrl Pts',(-0.12648796685852,-0.0116483513064931,
0.0600681629389771));
#18216=CARTESIAN_POINT('Ctrl Pts',(-0.125028206814926,-0.0231743653405588,
0.0607943585160125));
#18217=CARTESIAN_POINT('Ctrl Pts',(-0.121921363946098,-0.034237873926493,
0.0615205540930479));
#18218=CARTESIAN_POINT('Ctrl Pts',(-0.110855003598394,-0.0736453296270277,
0.0641072127293806));
#18219=CARTESIAN_POINT('Ctrl Pts',(-0.0788915213442898,-0.107184815251071,
0.0666938713657133));
#18220=CARTESIAN_POINT('Ctrl Pts',(-0.0400617348236378,-0.120133683626334,
0.069280530002046));
#18221=CARTESIAN_POINT('Ctrl Pts',(-0.00123194830298627,-0.133082552001597,
0.0718671886383786));
#18222=CARTESIAN_POINT('Ctrl Pts',(0.0444641424842127,-0.125440803128081,
0.0744538472747112));
#18223=CARTESIAN_POINT('Ctrl Pts',(0.0769682295152699,-0.100563001286921,
0.0770405059110438));
#18224=CARTESIAN_POINT('Ctrl Pts',(0.109472316546327,-0.0756851994457607,
0.0796271645473764));
#18225=CARTESIAN_POINT('Ctrl Pts',(0.128784399821243,-0.0335713446369571,
0.0822138231837091));
#18226=CARTESIAN_POINT('Ctrl Pts',(0.126427276285523,0.00729262199647547,
0.0848004818200417));
#18227=CARTESIAN_POINT('Ctrl Pts',(0.124070152749803,0.0481565886299079,
0.0873871404563744));
#18228=CARTESIAN_POINT('Ctrl Pts',(0.100043822403448,0.0877706670879697,
0.0899737990927071));
#18229=CARTESIAN_POINT('Ctrl Pts',(0.0648947831756147,0.108746049780439,
0.0925604577290397));
#18230=CARTESIAN_POINT('Ctrl Pts',(0.0297457439477817,0.129721432472907,
0.0951471163653723));
#18231=CARTESIAN_POINT('Ctrl Pts',(-0.0165260041615291,0.132058119399784,
0.0977337750017049));
#18232=CARTESIAN_POINT('Ctrl Pts',(-0.0536093211433369,0.114730442741844,
0.100320433638038));
#18233=CARTESIAN_POINT('Ctrl Pts',(-0.0906926381251451,0.0974027660839045,
0.10290709227437));
#18234=CARTESIAN_POINT('Ctrl Pts',(-0.11858752397945,0.0604107258411485,
0.105493750910703));
#18235=CARTESIAN_POINT('Ctrl Pts',(-0.12504939731921,0.0199921027543164,
0.108080409547035));
#18236=CARTESIAN_POINT('Ctrl Pts',(-0.126099919499473,0.0134211506765118,
0.108500928818671));
#18237=CARTESIAN_POINT('Ctrl Pts',(-0.126583971845017,0.00675963476331471,
0.108921448090306));
#18238=CARTESIAN_POINT('Ctrl Pts',(-0.126529791093031,9.025049583615E-5,
0.109341967361942));
#18239=CARTESIAN_POINT('Origin',(0.,0.,0.12));
#18240=CARTESIAN_POINT('',(-0.126296536029262,-6.10717992316628E-5,0.159341967361942));
#18241=CARTESIAN_POINT('',(-0.126453631260982,-0.000102348163238207,0.145658032638058));
#18242=CARTESIAN_POINT('',(-0.12645,1.54856587752183E-17,0.12));
#18243=CARTESIAN_POINT('Ctrl Pts',(-0.126453631260982,-0.000102348163238207,
0.145658032638058));
#18244=CARTESIAN_POINT('Ctrl Pts',(-0.126183364177612,0.031552920325249,
0.143665210546026));
#18245=CARTESIAN_POINT('Ctrl Pts',(-0.114073771100105,0.0633928690595716,
0.141672388453994));
#18246=CARTESIAN_POINT('Ctrl Pts',(-0.0925489356314354,0.0864391430514358,
0.139679566361962));
#18247=CARTESIAN_POINT('Ctrl Pts',(-0.0646099631645552,0.116352924063146,
0.13709290772563));
#18248=CARTESIAN_POINT('Ctrl Pts',(-0.0208084524006029,0.131451366650306,
0.134506249089297));
#18249=CARTESIAN_POINT('Ctrl Pts',(0.0196287675426836,0.125106932552633,
0.131919590452964));
#18250=CARTESIAN_POINT('Ctrl Pts',(0.0600659874859703,0.11876249845496,
0.129332931816632));
#18251=CARTESIAN_POINT('Ctrl Pts',(0.097138916608591,0.0909751876724545,
0.126746273180299));
#18252=CARTESIAN_POINT('Ctrl Pts',(0.114574233156503,0.0539423598350403,
0.124159614543967));
#18253=CARTESIAN_POINT('Ctrl Pts',(0.132009549704415,0.0169095319976262,
0.121572955907634));
#18254=CARTESIAN_POINT('Ctrl Pts',(0.129807253677619,-0.0293688128946969,
0.118986297271301));
#18255=CARTESIAN_POINT('Ctrl Pts',(0.108934072954415,-0.0645786240759305,
0.116399638634969));
#18256=CARTESIAN_POINT('Ctrl Pts',(0.0880608922312115,-0.099788435257164,
0.113812979998636));
#18257=CARTESIAN_POINT('Ctrl Pts',(0.0485168268116012,-0.123929712727308,
0.111226321362303));
#18258=CARTESIAN_POINT('Ctrl Pts',(0.00765986125275547,-0.126405537442516,
0.108639662725971));
#18259=CARTESIAN_POINT('Ctrl Pts',(-0.0331971043060904,-0.128881362157723,
0.106053004089638));
#18260=CARTESIAN_POINT('Ctrl Pts',(-0.0753669700041717,-0.109691734117994,
0.103466345453305));
#18261=CARTESIAN_POINT('Ctrl Pts',(-0.100339039978837,-0.0772600332835736,
0.100879686816973));
#18262=CARTESIAN_POINT('Ctrl Pts',(-0.117142637704978,-0.0554368822612891,
0.0991391354240014));
#18263=CARTESIAN_POINT('Ctrl Pts',(-0.126159269908366,-0.0276178718881664,
0.0973985840310299));
#18264=CARTESIAN_POINT('Ctrl Pts',(-0.126349242904067,8.85860673823967E-5,
0.0956580326380584));
#18265=CARTESIAN_POINT('Ctrl Pts',(-0.126529791093031,9.025049583615E-5,
0.109341967361942));
#18266=CARTESIAN_POINT('Ctrl Pts',(-0.126250700293628,-0.0342644551610371,
0.111508106726639));
#18267=CARTESIAN_POINT('Ctrl Pts',(-0.111690189779818,-0.0688279388928191,
0.113674246091336));
#18268=CARTESIAN_POINT('Ctrl Pts',(-0.0867076257192948,-0.092297473337895,
0.115840385456033));
#18269=CARTESIAN_POINT('Ctrl Pts',(-0.0568751199544048,-0.120323220412367,
0.118427044092366));
#18270=CARTESIAN_POINT('Ctrl Pts',(-0.0121812475994092,-0.132529508630403,
0.121013702728699));
#18271=CARTESIAN_POINT('Ctrl Pts',(0.0277554439013372,-0.123558363290506,
0.123600361365031));
#18272=CARTESIAN_POINT('Ctrl Pts',(0.0676921354020838,-0.114587217950609,
0.126187020001364));
#18273=CARTESIAN_POINT('Ctrl Pts',(0.102871646048582,-0.0844386390527785,
0.128773678637697));
#18274=CARTESIAN_POINT('Ctrl Pts',(0.117851793294146,-0.0463464242807743,
0.131360337274029));
#18275=CARTESIAN_POINT('Ctrl Pts',(0.13283194053971,-0.00825420950877041,
0.133946995910362));
#18276=CARTESIAN_POINT('Ctrl Pts',(0.127612724384341,0.0377816411374068,
0.136533654546694));
#18277=CARTESIAN_POINT('Ctrl Pts',(0.104485135941302,0.0715534408109559,
0.139120313183027));
#18278=CARTESIAN_POINT('Ctrl Pts',(0.0813575474982633,0.105325240484505,
0.14170697181936));
#18279=CARTESIAN_POINT('Ctrl Pts',(0.0403215867675544,0.126832989185426,
0.144293630455692));
#18280=CARTESIAN_POINT('Ctrl Pts',(-0.000609841963000384,0.126635909896556,
0.146880289092025));
#18281=CARTESIAN_POINT('Ctrl Pts',(-0.0415412706935549,0.126438830607686,
0.149466947728358));
#18282=CARTESIAN_POINT('Ctrl Pts',(-0.0823681674239554,0.104536923329025,
0.15205360636469));
#18283=CARTESIAN_POINT('Ctrl Pts',(-0.10516942503222,0.0705438627883669,
0.154640265001023));
#18284=CARTESIAN_POINT('Ctrl Pts',(-0.118984510025511,0.0499477610899654,
0.156207499121329));
#18285=CARTESIAN_POINT('Ctrl Pts',(-0.126182304652747,0.0249129445447297,
0.157774733241635));
#18286=CARTESIAN_POINT('Ctrl Pts',(-0.126296536029262,-6.10717992316628E-5,
0.159341967361942));
#18287=CARTESIAN_POINT('Origin',(0.,0.,0.12));
#18288=CARTESIAN_POINT('',(-0.126625441102054,2.7778768752873E-5,0.209341967361942));
#18289=CARTESIAN_POINT('',(-0.126471935391749,0.000101176582396995,0.195658032638058));
#18290=CARTESIAN_POINT('',(-0.12645,1.54856587752183E-17,0.12));
#18291=CARTESIAN_POINT('',(0.0958116152722397,0.0825211298936481,0.24));
#18292=CARTESIAN_POINT('Ctrl Pts',(-0.126625441102054,2.7778768752873E-5,
0.209341967361942));
#18293=CARTESIAN_POINT('Ctrl Pts',(-0.126482885932031,-0.0388928622545336,
0.21180133566563));
#18294=CARTESIAN_POINT('Ctrl Pts',(-0.107125339127294,-0.077921419747323,
0.214260703969318));
#18295=CARTESIAN_POINT('Ctrl Pts',(-0.0759952538809665,-0.101287130411732,
0.216720072273006));
#18296=CARTESIAN_POINT('Ctrl Pts',(-0.0432539585932993,-0.12586218783339,
0.219306730909339));
#18297=CARTESIAN_POINT('Ctrl Pts',(0.0025100419330305,-0.133111106253138,
0.221893389545672));
#18298=CARTESIAN_POINT('Ctrl Pts',(0.0412155518054008,-0.119764891216682,
0.224480048182004));
#18299=CARTESIAN_POINT('Ctrl Pts',(0.0799210616777711,-0.106418676180227,
0.227066706818337));
#18300=CARTESIAN_POINT('Ctrl Pts',(0.111568080896182,-0.072477327687567,
0.229653365454669));
#18301=CARTESIAN_POINT('Ctrl Pts',(0.122246574267713,-0.0330282462555153,
0.232240024091002));
#18302=CARTESIAN_POINT('Ctrl Pts',(0.132925067639245,0.00642083517653631,
0.234826682727335));
#18303=CARTESIAN_POINT('Ctrl Pts',(0.122635035163896,0.0513776495479799,
0.237413341363667));
#18304=CARTESIAN_POINT('Ctrl Pts',(0.0958116152722397,0.0825211298936481,
0.24));
#18305=CARTESIAN_POINT('',(-0.0959791030802601,0.0826138105732953,0.24));
#18306=CARTESIAN_POINT('Origin',(0.,0.,0.24));
#18307=CARTESIAN_POINT('Ctrl Pts',(-0.0959791030802601,0.0826138105732953,
0.24));
#18308=CARTESIAN_POINT('Ctrl Pts',(-0.0710417758635208,0.111296717646776,
0.237599759089979));
#18309=CARTESIAN_POINT('Ctrl Pts',(-0.0322351762885183,0.128218895525122,
0.235199518179958));
#18310=CARTESIAN_POINT('Ctrl Pts',(0.00571352152256588,0.126497857083363,
0.232799277269937));
#18311=CARTESIAN_POINT('Ctrl Pts',(0.0466095526337785,0.124643152028446,
0.230212618633605));
#18312=CARTESIAN_POINT('Ctrl Pts',(0.0865092470399708,0.101136876245298,
0.227625959997272));
#18313=CARTESIAN_POINT('Ctrl Pts',(0.107920636628548,0.0662586835305903,
0.225039301360939));
#18314=CARTESIAN_POINT('Ctrl Pts',(0.129332026217125,0.0313804908158828,
0.222452642724607));
#18315=CARTESIAN_POINT('Ctrl Pts',(0.132255110988087,-0.014869618830384,
0.219865984088274));
#18316=CARTESIAN_POINT('Ctrl Pts',(0.115395215428634,-0.0521699181865619,
0.217279325451942));
#18317=CARTESIAN_POINT('Ctrl Pts',(0.0985353198691812,-0.0894702175427398,
0.214692666815609));
#18318=CARTESIAN_POINT('Ctrl Pts',(0.0618924439793129,-0.117820706608829,
0.212106008179276));
#18319=CARTESIAN_POINT('Ctrl Pts',(0.0215571925812854,-0.12478734248304,
0.209519349542944));
#18320=CARTESIAN_POINT('Ctrl Pts',(-0.0187780588167422,-0.13175397835725,
0.206932690906611));
#18321=CARTESIAN_POINT('Ctrl Pts',(-0.0628056857229291,-0.117336761039583,
0.204346032270278));
#18322=CARTESIAN_POINT('Ctrl Pts',(-0.0912027768750998,-0.0878586653637446,
0.201759373633946));
#18323=CARTESIAN_POINT('Ctrl Pts',(-0.113530209130371,-0.0646812849521466,
0.199725593301983));
#18324=CARTESIAN_POINT('Ctrl Pts',(-0.126194825294183,-0.0321932513395888,
0.197691812970021));
#18325=CARTESIAN_POINT('Ctrl Pts',(-0.126471935391749,0.000101176582396995,
0.195658032638058));
#18326=CARTESIAN_POINT('Origin',(0.,0.,0.350421172358873));
#18327=CARTESIAN_POINT('',(-0.154453350152392,-8.79343647196378E-5,0.0295788276411275));
#18328=CARTESIAN_POINT('',(-0.15422847552802,0.000108763211052777,0.025421172358873));
#18329=CARTESIAN_POINT('',(-0.1543,-1.01731279388251E-15,0.350421172358873));
#18330=CARTESIAN_POINT('',(0.15408394018464,-0.00816268198427004,0.));
#18331=CARTESIAN_POINT('Ctrl Pts',(-0.15422847552802,0.000108763211052763,
0.025421172358873));
#18332=CARTESIAN_POINT('Ctrl Pts',(-0.154338737393477,0.0139570514561378,
0.0247074241482466));
#18333=CARTESIAN_POINT('Ctrl Pts',(-0.146387882101843,0.0778735560251454,
0.0214070173012875));
#18334=CARTESIAN_POINT('Ctrl Pts',(-0.0581466660421577,0.171532975008042,
0.0155199518179959));
#18335=CARTESIAN_POINT('Ctrl Pts',(0.109502662757235,0.144085240745689,
0.00775997590899784));
#18336=CARTESIAN_POINT('Ctrl Pts',(0.156737212705124,0.0419221657566679,
0.00258665863633264));
#18337=CARTESIAN_POINT('Ctrl Pts',(0.15408394018464,-0.00816268198427004,
0.));
#18338=CARTESIAN_POINT('',(0.129620323775263,-0.0841289546921688,3.62607491890453E-17));
#18339=CARTESIAN_POINT('Origin',(0.,0.,0.));
#18340=CARTESIAN_POINT('Ctrl Pts',(-0.154453350152392,-8.7934364719636E-5,
0.0295788276411275));
#18341=CARTESIAN_POINT('Ctrl Pts',(-0.154150470777978,0.0441115087317509,
0.0272927766101045));
#18342=CARTESIAN_POINT('Ctrl Pts',(-0.111454882743928,0.138841433785012,
0.0224200669427489));
#18343=CARTESIAN_POINT('Ctrl Pts',(0.0476444145610997,0.174632482457551,
0.0149606986390605));
#18344=CARTESIAN_POINT('Ctrl Pts',(0.168251138196633,0.0613688951001999,
0.0073871404563744));
#18345=CARTESIAN_POINT('Ctrl Pts',(0.154676764047789,-0.0451013867871701,
0.00240024091002087));
#18346=CARTESIAN_POINT('Ctrl Pts',(0.129620323775263,-0.0841289546921688,
1.57209315010398E-17));
#18347=CARTESIAN_POINT('Origin',(0.,0.,0.350421172358873));
#18348=CARTESIAN_POINT('',(-0.154177051641736,0.000108096719625833,0.0795788276411275));
#18349=CARTESIAN_POINT('',(-0.154234284709463,-0.000121519309271207,0.075421172358873));
#18350=CARTESIAN_POINT('',(-0.1543,-1.01731279388251E-15,0.350421172358873));
#18351=CARTESIAN_POINT('Ctrl Pts',(-0.154234284709463,-0.000121519309271208,
0.0754211723588731));
#18352=CARTESIAN_POINT('Ctrl Pts',(-0.153947235272697,0.0359820467524117,
0.0735607092995758));
#18353=CARTESIAN_POINT('Ctrl Pts',(-0.123557126730793,0.122717061869437,
0.0691135876039459));
#18354=CARTESIAN_POINT('Ctrl Pts',(0.0191012565771036,0.180005302104073,
0.0620798072719832));
#18355=CARTESIAN_POINT('Ctrl Pts',(0.159724738700703,0.0851738948996701,
0.0543198313629854));
#18356=CARTESIAN_POINT('Ctrl Pts',(0.160113920417758,-0.0844204212478698,
0.0465598554539874));
#18357=CARTESIAN_POINT('Ctrl Pts',(0.0199582426985643,-0.179924098035372,
0.0387998795449896));
#18358=CARTESIAN_POINT('Ctrl Pts',(-0.123251388539896,-0.123176028715441,
0.0317536518466181));
#18359=CARTESIAN_POINT('Ctrl Pts',(-0.153939142967466,-0.0362298265692857,
0.0272940827845792));
#18360=CARTESIAN_POINT('Ctrl Pts',(-0.15422847552802,0.000108763211052763,
0.025421172358873));
#18361=CARTESIAN_POINT('Ctrl Pts',(-0.154177051641736,0.000108096719625859,
0.0795788276411275));
#18362=CARTESIAN_POINT('Ctrl Pts',(-0.154289739603949,0.0165429814548096,
0.0787327203977663));
#18363=CARTESIAN_POINT('Ctrl Pts',(-0.144420757340354,0.0830897487115299,
0.0752999545180725));
#18364=CARTESIAN_POINT('Ctrl Pts',(-0.0494457976037486,0.174130301808973,
0.0692805300020459));
#18365=CARTESIAN_POINT('Ctrl Pts',(0.11640175885633,0.13862511662766,0.061520554093048));
#18366=CARTESIAN_POINT('Ctrl Pts',(0.18005704388064,-0.0185795878987759,
0.0537605781840501));
#18367=CARTESIAN_POINT('Ctrl Pts',(0.0856431484406112,-0.159474177462153,
0.0460006022750521));
#18368=CARTESIAN_POINT('Ctrl Pts',(-0.0839657292871194,-0.160363143120653,
0.0382406263660544));
#18369=CARTESIAN_POINT('Ctrl Pts',(-0.151599316432495,-0.0616831513139142,
0.0327667014880793));
#18370=CARTESIAN_POINT('Ctrl Pts',(-0.154493177716258,-0.00590000442131094,
0.0298794352464371));
#18371=CARTESIAN_POINT('Ctrl Pts',(-0.154453350152392,-8.7934364719636E-5,
0.0295788276411275));
#18372=CARTESIAN_POINT('Origin',(0.,0.,0.350421172358873));
#18373=CARTESIAN_POINT('',(-0.154304431028624,-0.000124889850439479,0.129578827641127));
#18374=CARTESIAN_POINT('',(-0.154397364694779,0.000110127730384366,0.125421172358873));
#18375=CARTESIAN_POINT('',(-0.1543,-1.01731279388251E-15,0.350421172358873));
#18376=CARTESIAN_POINT('Ctrl Pts',(-0.154397364694779,0.000110127730384357,
0.125421172358873));
#18377=CARTESIAN_POINT('Ctrl Pts',(-0.154463478494948,0.00824841157753406,
0.125000653087238));
#18378=CARTESIAN_POINT('Ctrl Pts',(-0.150239588102603,0.0663774823757793,
0.121993475179269));
#18379=CARTESIAN_POINT('Ctrl Pts',(-0.0766286530280003,0.163994611436961,
0.116399638634969));
#18380=CARTESIAN_POINT('Ctrl Pts',(0.0927599764682439,0.155440618724813,
0.108639662725971));
#18381=CARTESIAN_POINT('Ctrl Pts',(0.180714016146597,0.0104239566588842,
0.100879686816973));
#18382=CARTESIAN_POINT('Ctrl Pts',(0.11001758793024,-0.143743725357685,
0.093119710907975));
#18383=CARTESIAN_POINT('Ctrl Pts',(-0.0572637123892103,-0.171718146500831,
0.0853597349989769));
#18384=CARTESIAN_POINT('Ctrl Pts',(-0.146220320052713,-0.0783754111826042,
0.0794602221492764));
#18385=CARTESIAN_POINT('Ctrl Pts',(-0.154346328875204,-0.0142138442593302,
0.0761473679359084));
#18386=CARTESIAN_POINT('Ctrl Pts',(-0.154234284709463,-0.000121519309271208,
0.0754211723588731));
#18387=CARTESIAN_POINT('Ctrl Pts',(-0.154304431028624,-0.000124889850439474,
0.129578827641127));
#18388=CARTESIAN_POINT('Ctrl Pts',(-0.153974638929265,0.0385022981904757,
0.127586005549095));
#18389=CARTESIAN_POINT('Ctrl Pts',(-0.120018027207353,0.127784966030512,
0.123006524820731));
#18390=CARTESIAN_POINT('Ctrl Pts',(0.0280571680938306,0.178826694862324,
0.115840385456033));
#18391=CARTESIAN_POINT('Ctrl Pts',(0.163771354656592,0.0771047007047774,
0.108080409547035));
#18392=CARTESIAN_POINT('Ctrl Pts',(0.155709331479018,-0.0923080778690166,
0.100320433638038));
#18393=CARTESIAN_POINT('Ctrl Pts',(0.0109489686262093,-0.180682908560435,
0.0925604577290397));
#18394=CARTESIAN_POINT('Ctrl Pts',(-0.126591758993125,-0.118094248159534,
0.0856465890634029));
#18395=CARTESIAN_POINT('Ctrl Pts',(-0.153945238013925,-0.0337005743957639,
0.0813193790340989));
#18396=CARTESIAN_POINT('Ctrl Pts',(-0.154177051641736,0.000108096719625859,
0.0795788276411275));
#18397=CARTESIAN_POINT('Origin',(0.,0.,0.350421172358873));
#18398=CARTESIAN_POINT('',(-0.154326766555531,0.000123460234585843,0.179578827641127));
#18399=CARTESIAN_POINT('',(-0.154112736333057,-7.45225671948511E-5,0.175421172358873));
#18400=CARTESIAN_POINT('',(-0.1543,-1.01731279388251E-15,0.350421172358873));
#18401=CARTESIAN_POINT('Ctrl Pts',(-0.154112736333057,-7.45225671948471E-5,
0.175421172358873));
#18402=CARTESIAN_POINT('Ctrl Pts',(-0.153973346049181,0.0303998999070902,
0.173853938238567));
#18403=CARTESIAN_POINT('Ctrl Pts',(-0.130694151755309,0.111367805862998,
0.169700045481928));
#18404=CARTESIAN_POINT('Ctrl Pts',(-0.000871711368246156,0.181012066871201,
0.162959494088956));
#18405=CARTESIAN_POINT('Ctrl Pts',(0.149350085565286,0.102277888352765,
0.155199518179958));
#18406=CARTESIAN_POINT('Ctrl Pts',(0.168456255263351,-0.0662471829332422,
0.14743954227096));
#18407=CARTESIAN_POINT('Ctrl Pts',(0.0396733728729688,-0.17661315503135,
0.139679566361963));
#18408=CARTESIAN_POINT('Ctrl Pts',(-0.115072782317819,-0.134350623919955,
0.1323401097246));
#18409=CARTESIAN_POINT('Ctrl Pts',(-0.154056805498669,-0.041811035439686,
0.12758731172357));
#18410=CARTESIAN_POINT('Ctrl Pts',(-0.154397364694779,0.000110127730384357,
0.125421172358873));
#18411=CARTESIAN_POINT('Ctrl Pts',(-0.154326766555531,0.000123460234585825,
0.179578827641127));
#18412=CARTESIAN_POINT('Ctrl Pts',(-0.154418689716183,0.0108361910665024,
0.179025949336757));
#18413=CARTESIAN_POINT('Ctrl Pts',(-0.148597337680631,0.071569631208062,
0.175886412396054));
#18414=CARTESIAN_POINT('Ctrl Pts',(-0.0683530255288039,0.167611467503216,
0.170160216819019));
#18415=CARTESIAN_POINT('Ctrl Pts',(0.100397202365132,0.150621028353064,
0.162400240910021));
#18416=CARTESIAN_POINT('Ctrl Pts',(0.18100910679194,0.00139719974911195,
0.154640265001023));
#18417=CARTESIAN_POINT('Ctrl Pts',(0.102711092909207,-0.149052183789333,
0.146880289092025));
#18418=CARTESIAN_POINT('Ctrl Pts',(-0.0657574679958034,-0.168648048308422,
0.139120313183027));
#18419=CARTESIAN_POINT('Ctrl Pts',(-0.148058381688037,-0.0731761882111772,
0.133353159366061));
#18420=CARTESIAN_POINT('Ctrl Pts',(-0.154402705029802,-0.0116353181791797,
0.130172664185428));
#18421=CARTESIAN_POINT('Ctrl Pts',(-0.154304431028624,-0.000124889850439474,
0.129578827641127));
#18422=CARTESIAN_POINT('Origin',(0.,0.,0.350421172358873));
#18423=CARTESIAN_POINT('',(-0.154128406284035,-0.000157308197905263,0.229578827641128));
#18424=CARTESIAN_POINT('',(-0.154514081154978,3.38969080117728E-5,0.225421172358873));
#18425=CARTESIAN_POINT('',(-0.1543,-1.01731279388251E-15,0.350421172358873));
#18426=CARTESIAN_POINT('',(-0.0398513841857245,-0.149064942821851,0.24));
#18427=CARTESIAN_POINT('Ctrl Pts',(-0.0398513841857245,-0.149064942821851,
0.24));
#18428=CARTESIAN_POINT('Ctrl Pts',(-0.0883048112969314,-0.136111285829332,
0.237413341363667));
#18429=CARTESIAN_POINT('Ctrl Pts',(-0.143745772087175,-0.0847488633265083,
0.233939617244043));
#18430=CARTESIAN_POINT('Ctrl Pts',(-0.154234229255939,-0.017399338864059,
0.230465893124419));
#18431=CARTESIAN_POINT('Ctrl Pts',(-0.154128406284035,-0.00015730819790527,
0.229578827641128));
#18432=CARTESIAN_POINT('',(0.0399565498027962,-0.149273502906638,0.24));
#18433=CARTESIAN_POINT('Origin',(0.,0.,0.24));
#18434=CARTESIAN_POINT('Ctrl Pts',(0.0399565498027963,-0.149273502906638,
0.24));
#18435=CARTESIAN_POINT('Ctrl Pts',(-0.00490373130458673,-0.161043406468747,
0.237599759089979));
#18436=CARTESIAN_POINT('Ctrl Pts',(-0.107666111297752,-0.141562671532916,
0.23274014987627));
#18437=CARTESIAN_POINT('Ctrl Pts',(-0.154340128899266,-0.0474588267763927,
0.227880540662561));
#18438=CARTESIAN_POINT('Ctrl Pts',(-0.154514081154978,3.3896908011755E-5,
0.225421172358873));
#18439=CARTESIAN_POINT('Origin',(0.,0.,0.350421172358873));
#18440=CARTESIAN_POINT('Ctrl Pts',(-0.154514081154978,3.3896908011755E-5,
0.225421172358873));
#18441=CARTESIAN_POINT('Ctrl Pts',(-0.154523084458981,0.00249199339844659,
0.225293882026228));
#18442=CARTESIAN_POINT('Ctrl Pts',(-0.153375868586475,0.0548933889046004,
0.222579933057251));
#18443=CARTESIAN_POINT('Ctrl Pts',(-0.0942515706791253,0.154556313135293,
0.217279325451942));
#18444=CARTESIAN_POINT('Ctrl Pts',(0.0750450248431312,0.164716481511431,
0.209519349542944));
#18445=CARTESIAN_POINT('Ctrl Pts',(0.178461260043253,0.0303012077178856,
0.201759373633945));
#18446=CARTESIAN_POINT('Ctrl Pts',(0.125203781387627,-0.130731709675357,
0.193999397724948));
#18447=CARTESIAN_POINT('Ctrl Pts',(-0.0379704533096903,-0.17698585337688,
0.18623942181595));
#18448=CARTESIAN_POINT('Ctrl Pts',(-0.141587477595567,-0.0899051669249145,
0.180046680027258));
#18449=CARTESIAN_POINT('Ctrl Pts',(-0.154203404262525,-0.019896942829432,
0.176440596874899));
#18450=CARTESIAN_POINT('Ctrl Pts',(-0.154112736333057,-7.45225671948471E-5,
0.175421172358873));
#18451=CARTESIAN_POINT('Ctrl Pts',(-0.154128406284035,-0.00015730819790527,
0.229578827641128));
#18452=CARTESIAN_POINT('Ctrl Pts',(-0.153925652370292,0.0328779499839183,
0.227879234488086));
#18453=CARTESIAN_POINT('Ctrl Pts',(-0.127638532780061,0.116591914860373,
0.223592982698713));
#18454=CARTESIAN_POINT('Ctrl Pts',(0.00818767200092134,0.180778621679153,
0.216720072273006));
#18455=CARTESIAN_POINT('Ctrl Pts',(0.154249898498561,0.0947283641859207,
0.208960096364008));
#18456=CARTESIAN_POINT('Ctrl Pts',(0.164950538597243,-0.0745810526211722,
0.201200120455011));
#18457=CARTESIAN_POINT('Ctrl Pts',(0.0308106631569891,-0.178364693496558,
0.193440144546012));
#18458=CARTESIAN_POINT('Ctrl Pts',(-0.118879635670858,-0.129347344159377,
0.186233046941385));
#18459=CARTESIAN_POINT('Ctrl Pts',(-0.153988624301243,-0.0392836590090855,
0.18161260797309));
#18460=CARTESIAN_POINT('Ctrl Pts',(-0.154326766555531,0.000123460234585825,
0.179578827641127));
#18461=CARTESIAN_POINT('Ctrl Pts',(0.0958116152722397,0.0825211298936481,
0.24));
#18462=CARTESIAN_POINT('Ctrl Pts',(0.122635035163896,0.0513776495479799,
0.237413341363667));
#18463=CARTESIAN_POINT('Ctrl Pts',(0.143215100114593,-0.0385359791949074,
0.232240024091002));
#18464=CARTESIAN_POINT('Ctrl Pts',(0.0482740424593604,-0.140360024672886,
0.224480048182004));
#18465=CARTESIAN_POINT('Ctrl Pts',(-0.0890179591196291,-0.118613269413641,
0.216720072273006));
#18466=CARTESIAN_POINT('Ctrl Pts',(-0.148173729266643,0.00709031985706173,
0.208960096364008));
#18467=CARTESIAN_POINT('Ctrl Pts',(-0.0772398646297824,0.126660050524678,
0.20120012045501));
#18468=CARTESIAN_POINT('Ctrl Pts',(0.0614999571705377,0.134986384232796,
0.193440144546013));
#18469=CARTESIAN_POINT('Ctrl Pts',(0.146250332679645,0.0248320655601208,
0.185680168637014));
#18470=CARTESIAN_POINT('Ctrl Pts',(0.102605431992647,-0.107135610424167,
0.177920192728017));
#18471=CARTESIAN_POINT('Ctrl Pts',(-0.0311170694815965,-0.145041225920327,
0.170160216819019));
#18472=CARTESIAN_POINT('Ctrl Pts',(-0.137521919612742,-0.0556176253575994,
0.162400240910021));
#18473=CARTESIAN_POINT('Ctrl Pts',(-0.123195064154356,0.0826350160503635,
0.154640265001023));
#18474=CARTESIAN_POINT('Ctrl Pts',(-0.000714373963154436,0.148340737886347,
0.146880289092025));
#18475=CARTESIAN_POINT('Ctrl Pts',(0.122393508228972,0.0838174917835845,
0.139120313183027));
#18476=CARTESIAN_POINT('Ctrl Pts',(0.138051156695079,-0.0542900601549481,
0.131360337274029));
#18477=CARTESIAN_POINT('Ctrl Pts',(0.032512624755586,-0.14473579684844,
0.123600361365031));
#18478=CARTESIAN_POINT('Ctrl Pts',(-0.101568992309399,-0.108116932194331,
0.115840385456033));
#18479=CARTESIAN_POINT('Ctrl Pts',(-0.146482409833755,0.0234186855983926,
0.108080409547036));
#18480=CARTESIAN_POINT('Ctrl Pts',(-0.0627977522708403,0.13439480632666,
0.100320433638038));
#18481=CARTESIAN_POINT('Ctrl Pts',(0.076017492057093,0.127384745546031,
0.0925604577290397));
#18482=CARTESIAN_POINT('Ctrl Pts',(0.148096483096158,0.00854251017184644,
0.0848004818200417));
#18483=CARTESIAN_POINT('Ctrl Pts',(0.0901602332714121,-0.117799054254564,
0.0770405059110438));
#18484=CARTESIAN_POINT('Ctrl Pts',(-0.0469280390901857,-0.140724300875114,
0.069280530002046));
#18485=CARTESIAN_POINT('Ctrl Pts',(-0.142818485852497,-0.0401058440029853,
0.0615205540930479));
#18486=CARTESIAN_POINT('Ctrl Pts',(-0.113326201176411,0.0957204333280909,
0.0537605781840501));
#18487=CARTESIAN_POINT('Ctrl Pts',(0.0156536221268617,0.147515686656254,
0.0460006022750521));
#18488=CARTESIAN_POINT('Ctrl Pts',(0.130895613795878,0.0698006416724775,
0.0382406263660543));
#18489=CARTESIAN_POINT('Ctrl Pts',(0.13121455111358,-0.0691831643991777,
0.0304806504570563));
#18490=CARTESIAN_POINT('Ctrl Pts',(0.0163559286405278,-0.147449139316739,
0.0227206745480584));
#18491=CARTESIAN_POINT('Ctrl Pts',(-0.112893560070904,-0.0962328986104914,
0.0149606986390606));
#18492=CARTESIAN_POINT('Ctrl Pts',(-0.142972035491037,0.0393992613429074,
0.00720072273006258));
#18493=CARTESIAN_POINT('Ctrl Pts',(-0.0476516261894416,0.140572551456688,
-0.000559253178935252));
#18494=CARTESIAN_POINT('Ctrl Pts',(0.0897382482543901,0.118078928660352,
-0.00831922908793326));
#18495=CARTESIAN_POINT('Ctrl Pts',(0.128447313976429,0.0343555272840613,
-0.0134925463605985));
#18496=CARTESIAN_POINT('Ctrl Pts',(0.126272937371016,-0.00668937872268922,
-0.0160792049969311));
#18497=CARTESIAN_POINT('Ctrl Pts',(0.102845629995666,0.0885794229410663,
0.245359734998977));
#18498=CARTESIAN_POINT('Ctrl Pts',(0.13163829265517,0.0551495423644061,
0.242773076362644));
#18499=CARTESIAN_POINT('Ctrl Pts',(0.153729244145676,-0.0413651001137901,
0.237599759089979));
#18500=CARTESIAN_POINT('Ctrl Pts',(0.0518180837997932,-0.150664563191773,
0.229839783180981));
#18501=CARTESIAN_POINT('Ctrl Pts',(-0.0955532172229155,-0.127321268762976,
0.222079807271983));
#18502=CARTESIAN_POINT('Ctrl Pts',(-0.159051911315084,0.00761085605850937,
0.214319831362985));
#18503=CARTESIAN_POINT('Ctrl Pts',(-0.0829104333128967,0.135958804728216,
0.206559855453988));
#18504=CARTESIAN_POINT('Ctrl Pts',(0.0660149797280689,0.144896416659008,
0.19879987954499));
#18505=CARTESIAN_POINT('Ctrl Pts',(0.156987308467515,0.0266551129460425,
0.191039903635992));
#18506=CARTESIAN_POINT('Ctrl Pts',(0.110138215124307,-0.11500097684123,
0.183279927726994));
#18507=CARTESIAN_POINT('Ctrl Pts',(-0.0334015307576278,-0.155689435072511,
0.175519951817996));
#18508=CARTESIAN_POINT('Ctrl Pts',(-0.147618098500879,-0.0597007962188336,
0.167759975908998));
#18509=CARTESIAN_POINT('Ctrl Pts',(-0.13223943620312,0.0887016700559064,
0.16));
#18510=CARTESIAN_POINT('Ctrl Pts',(-0.000766819764851659,0.159231180881298,
0.152240024091002));
#18511=CARTESIAN_POINT('Ctrl Pts',(0.131379034007743,0.0899709573066447,
0.144480048182004));
#18512=CARTESIAN_POINT('Ctrl Pts',(0.14818618955117,-0.0582757677477129,
0.136720072273006));
#18513=CARTESIAN_POINT('Ctrl Pts',(0.0348995407947136,-0.15536158290941,
0.128960096364009));
#18514=CARTESIAN_POINT('Ctrl Pts',(-0.109025685167754,-0.116054342400242,
0.12120012045501));
#18515=CARTESIAN_POINT('Ctrl Pts',(-0.157236423577976,0.0251379696208395,
0.113440144546013));
#18516=CARTESIAN_POINT('Ctrl Pts',(-0.0674080525232269,0.144261408030094,
0.105680168637014));
#18517=CARTESIAN_POINT('Ctrl Pts',(0.0815983201941432,0.136736703272292,
0.0979201927280168));
#18518=CARTESIAN_POINT('Ctrl Pts',(0.158968994112971,0.00916965900085902,
0.0901602168190187));
#18519=CARTESIAN_POINT('Ctrl Pts',(0.0967793514910216,-0.126447277955604,
0.0824002409100209));
#18520=CARTESIAN_POINT('Ctrl Pts',(-0.0503732635231939,-0.151055582750353,
0.0746402650010229));
#18521=CARTESIAN_POINT('Ctrl Pts',(-0.15330351242688,-0.0430502166284845,
0.066880289092025));
#18522=CARTESIAN_POINT('Ctrl Pts',(-0.121646050135849,0.102747753924341,
0.0591203131830272));
#18523=CARTESIAN_POINT('Ctrl Pts',(0.0168028336102756,0.158345558472194,
0.0513603372740292));
#18524=CARTESIAN_POINT('Ctrl Pts',(0.140505322097486,0.074925059414875,
0.0436003613650313));
#18525=CARTESIAN_POINT('Ctrl Pts',(0.140847674214973,-0.0742622500154084,
0.0358403854560334));
#18526=CARTESIAN_POINT('Ctrl Pts',(0.0175566999932067,-0.158274125556283,
0.0280804095470355));
#18527=CARTESIAN_POINT('Ctrl Pts',(-0.121181646661057,-0.103297841872129,
0.0203204336380376));
#18528=CARTESIAN_POINT('Ctrl Pts',(-0.153468334920127,0.0422917601656304,
0.0125604577290396));
#18529=CARTESIAN_POINT('Ctrl Pts',(-0.0511499728070136,0.150892692640473,
0.00480048182004178));
#18530=CARTESIAN_POINT('Ctrl Pts',(0.0963263864220051,0.126747699355464,
-0.00295949408895622));
#18531=CARTESIAN_POINT('Ctrl Pts',(0.137877280219327,0.0368777401082635,
-0.00813281136162143));
#18532=CARTESIAN_POINT('Ctrl Pts',(0.135543271642224,-0.00718047980988283,
-0.0107194699979541));
#18533=CARTESIAN_POINT('Ctrl Pts',(0.109879644719093,0.0946377159884845,
0.250719469997954));
#18534=CARTESIAN_POINT('Ctrl Pts',(0.140641550146443,0.0589214351808321,
0.248132811361621));
#18535=CARTESIAN_POINT('Ctrl Pts',(0.164243388176759,-0.0441942210326729,
0.242959494088956));
#18536=CARTESIAN_POINT('Ctrl Pts',(0.055362125140226,-0.160969101710661,
0.235199518179958));
#18537=CARTESIAN_POINT('Ctrl Pts',(-0.102088475326202,-0.13602926811231,
0.227439542270961));
#18538=CARTESIAN_POINT('Ctrl Pts',(-0.169930093363525,0.00813139225995705,
0.219679566361962));
#18539=CARTESIAN_POINT('Ctrl Pts',(-0.0885810019960112,0.145257558931755,
0.211919590452965));
#18540=CARTESIAN_POINT('Ctrl Pts',(0.0705300022856002,0.154806449085219,
0.204159614543967));
#18541=CARTESIAN_POINT('Ctrl Pts',(0.167724284255384,0.0284781603319641,
0.196399638634969));
#18542=CARTESIAN_POINT('Ctrl Pts',(0.117670998255967,-0.122866343258294,
0.188639662725971));
#18543=CARTESIAN_POINT('Ctrl Pts',(-0.0356859920336591,-0.166337644224695,
0.180879686816973));
#18544=CARTESIAN_POINT('Ctrl Pts',(-0.157714277389017,-0.0637839670800676,
0.173119710907975));
#18545=CARTESIAN_POINT('Ctrl Pts',(-0.141283808251885,0.0947683240614489,
0.165359734998977));
#18546=CARTESIAN_POINT('Ctrl Pts',(-0.000819265566548849,0.17012162387625,
0.157599759089979));
#18547=CARTESIAN_POINT('Ctrl Pts',(0.140364559786514,0.0961244228297045,
0.149839783180981));
#18548=CARTESIAN_POINT('Ctrl Pts',(0.158321222407261,-0.0622614753404775,
0.142079807271983));
#18549=CARTESIAN_POINT('Ctrl Pts',(0.0372864568338413,-0.16598736897038,
0.134319831362986));
#18550=CARTESIAN_POINT('Ctrl Pts',(-0.116482378026109,-0.123991752606152,
0.126559855453987));
#18551=CARTESIAN_POINT('Ctrl Pts',(-0.167990437322196,0.0268572536432864,
0.11879987954499));
#18552=CARTESIAN_POINT('Ctrl Pts',(-0.0720183527756138,0.154128009733527,
0.111039903635992));
#18553=CARTESIAN_POINT('Ctrl Pts',(0.0871791483311938,0.146088660998552,
0.103279927726994));
#18554=CARTESIAN_POINT('Ctrl Pts',(0.169841505129784,0.00979680782987164,
0.0955199518179957));
#18555=CARTESIAN_POINT('Ctrl Pts',(0.103398469710631,-0.135095501656644,
0.0877599759089979));
#18556=CARTESIAN_POINT('Ctrl Pts',(-0.0538184879562023,-0.161386864625592,
0.08));
#18557=CARTESIAN_POINT('Ctrl Pts',(-0.163788539001263,-0.0459945892539838,
0.0722400240910021));
#18558=CARTESIAN_POINT('Ctrl Pts',(-0.129965899095288,0.10977507452059,
0.0644800481820042));
#18559=CARTESIAN_POINT('Ctrl Pts',(0.0179520450936897,0.169175430288133,
0.0567200722730062));
#18560=CARTESIAN_POINT('Ctrl Pts',(0.150115030399095,0.0800494771572726,
0.0489600963640084));
#18561=CARTESIAN_POINT('Ctrl Pts',(0.150480797316365,-0.0793413356316391,
0.0412001204550104));
#18562=CARTESIAN_POINT('Ctrl Pts',(0.0187574713458855,-0.169099111795828,
0.0334401445460125));
#18563=CARTESIAN_POINT('Ctrl Pts',(-0.129469733251211,-0.110362785133767,
0.0256801686370146));
#18564=CARTESIAN_POINT('Ctrl Pts',(-0.163964634349217,0.0451842589883535,
0.0179201927280167));
#18565=CARTESIAN_POINT('Ctrl Pts',(-0.0546483194245858,0.161212833824257,
0.0101602168190188));
#18566=CARTESIAN_POINT('Ctrl Pts',(0.10291452458962,0.135416470050577,0.00240024091002082));
#18567=CARTESIAN_POINT('Ctrl Pts',(0.147307246462226,0.0393999529324658,
-0.00277307636264439));
#18568=CARTESIAN_POINT('Ctrl Pts',(0.144813605913432,-0.00767158089707644,
-0.00535973499897704));
#18569=CARTESIAN_POINT('Ctrl Pts',(0.116913659442519,0.100696009035903,
0.256079204996931));
#18570=CARTESIAN_POINT('Ctrl Pts',(0.149644807637716,0.0626933279972582,
0.253492546360598));
#18571=CARTESIAN_POINT('Ctrl Pts',(0.174757532207842,-0.0470233419515556,
0.248319229087933));
#18572=CARTESIAN_POINT('Ctrl Pts',(0.0589061664806588,-0.171273640229548,
0.240559253178935));
#18573=CARTESIAN_POINT('Ctrl Pts',(-0.108623733429488,-0.144737267461644,
0.232799277269938));
#18574=CARTESIAN_POINT('Ctrl Pts',(-0.180808275411966,0.00865192846140473,
0.225039301360939));
#18575=CARTESIAN_POINT('Ctrl Pts',(-0.0942515706791253,0.154556313135293,
0.217279325451942));
#18576=CARTESIAN_POINT('Ctrl Pts',(0.0750450248431312,0.164716481511431,
0.209519349542944));
#18577=CARTESIAN_POINT('Ctrl Pts',(0.178461260043253,0.0303012077178856,
0.201759373633945));
#18578=CARTESIAN_POINT('Ctrl Pts',(0.125203781387627,-0.130731709675357,
0.193999397724948));
#18579=CARTESIAN_POINT('Ctrl Pts',(-0.0379704533096903,-0.17698585337688,
0.18623942181595));
#18580=CARTESIAN_POINT('Ctrl Pts',(-0.167810456277154,-0.0678671379413016,
0.178479445906952));
#18581=CARTESIAN_POINT('Ctrl Pts',(-0.150328180300649,0.100834978066992,
0.170719469997954));
#18582=CARTESIAN_POINT('Ctrl Pts',(-0.000871711368246156,0.181012066871201,
0.162959494088956));
#18583=CARTESIAN_POINT('Ctrl Pts',(0.149350085565286,0.102277888352765,
0.155199518179958));
#18584=CARTESIAN_POINT('Ctrl Pts',(0.168456255263351,-0.0662471829332422,
0.14743954227096));
#18585=CARTESIAN_POINT('Ctrl Pts',(0.0396733728729688,-0.17661315503135,
0.139679566361963));
#18586=CARTESIAN_POINT('Ctrl Pts',(-0.123939070884463,-0.131929162812062,
0.131919590452964));
#18587=CARTESIAN_POINT('Ctrl Pts',(-0.178744451066417,0.0285765376657333,
0.124159614543967));
#18588=CARTESIAN_POINT('Ctrl Pts',(-0.0766286530280003,0.163994611436961,
0.116399638634969));
#18589=CARTESIAN_POINT('Ctrl Pts',(0.0927599764682439,0.155440618724813,
0.108639662725971));
#18590=CARTESIAN_POINT('Ctrl Pts',(0.180714016146597,0.0104239566588842,
0.100879686816973));
#18591=CARTESIAN_POINT('Ctrl Pts',(0.11001758793024,-0.143743725357685,
0.093119710907975));
#18592=CARTESIAN_POINT('Ctrl Pts',(-0.0572637123892103,-0.171718146500831,
0.0853597349989769));
#18593=CARTESIAN_POINT('Ctrl Pts',(-0.174273565575645,-0.048938961879483,
0.0775997590899791));
#18594=CARTESIAN_POINT('Ctrl Pts',(-0.138285748054726,0.11680239511684,
0.0698397831809812));
#18595=CARTESIAN_POINT('Ctrl Pts',(0.0191012565771036,0.180005302104073,
0.0620798072719832));
#18596=CARTESIAN_POINT('Ctrl Pts',(0.159724738700703,0.0851738948996701,
0.0543198313629854));
#18597=CARTESIAN_POINT('Ctrl Pts',(0.160113920417758,-0.0844204212478698,
0.0465598554539874));
#18598=CARTESIAN_POINT('Ctrl Pts',(0.0199582426985643,-0.179924098035372,
0.0387998795449896));
#18599=CARTESIAN_POINT('Ctrl Pts',(-0.137757819841364,-0.117427728395404,
0.0310399036359917));
#18600=CARTESIAN_POINT('Ctrl Pts',(-0.174460933778308,0.0480767578110765,
0.0232799277269937));
#18601=CARTESIAN_POINT('Ctrl Pts',(-0.0581466660421577,0.171532975008042,
0.0155199518179959));
#18602=CARTESIAN_POINT('Ctrl Pts',(0.109502662757235,0.144085240745689,
0.00775997590899784));
#18603=CARTESIAN_POINT('Ctrl Pts',(0.156737212705124,0.0419221657566679,
0.00258665863633264));
#18604=CARTESIAN_POINT('Ctrl Pts',(0.15408394018464,-0.00816268198427004,
0.));
#18605=CARTESIAN_POINT('Ctrl Pts',(0.15408394018464,-0.00816268198427004,
0.));
#18606=CARTESIAN_POINT('Ctrl Pts',(0.153697863146473,0.00250812953454787,
1.45220469349306E-17));
#18607=CARTESIAN_POINT('Ctrl Pts',(0.152123106309386,0.0130673133993916,
-2.32988231788825E-17));
#18608=CARTESIAN_POINT('Ctrl Pts',(0.149466152202855,0.0233620190894148,
-6.07153216591882E-17));
#18609=CARTESIAN_POINT('Ctrl Pts',(0.14793019248835,0.0293132898222067,
-8.23454409684948E-17));
#18610=CARTESIAN_POINT('Ctrl Pts',(0.146031563681721,0.0351760135160456,
3.17823908273165E-17));
#18611=CARTESIAN_POINT('Ctrl Pts',(0.143784059453749,0.0409171473780902,
6.24500451351651E-17));
#18612=CARTESIAN_POINT('Ctrl Pts',(0.142595904075608,0.0439522291322952,
7.86626679846993E-17));
#18613=CARTESIAN_POINT('Ctrl Pts',(0.141309213132582,0.0469553015723855,
1.03399090950918E-16));
#18614=CARTESIAN_POINT('Ctrl Pts',(0.13992871365498,0.0499144025840292,
1.00613961606655E-16));
#18615=CARTESIAN_POINT('Ctrl Pts',(0.135493978469587,0.0594202586791481,
9.16669744478229E-17));
#18616=CARTESIAN_POINT('Ctrl Pts',(0.130119641392827,0.0684241765595774,
5.76730757846686E-17));
#18617=CARTESIAN_POINT('Ctrl Pts',(0.123887660540245,0.0767683201192124,
1.38777878078145E-16));
#18618=CARTESIAN_POINT('Ctrl Pts',(0.120656388342022,0.0810947453345699,
1.808305895663E-16));
#18619=CARTESIAN_POINT('Ctrl Pts',(0.117193874983239,0.0852432898306738,
1.062697842984E-16));
#18620=CARTESIAN_POINT('Ctrl Pts',(0.11350808038867,0.0891875047540603,
1.14491749414469E-16));
#18621=CARTESIAN_POINT('Ctrl Pts',(0.110158526423333,0.0927719043720516,
1.21963656801269E-16));
#18622=CARTESIAN_POINT('Ctrl Pts',(0.106618991420749,0.0961915975683434,
1.17223950247179E-16));
#18623=CARTESIAN_POINT('Ctrl Pts',(0.102922970874274,0.0994011657423757,
1.02348685082632E-16));
#18624=CARTESIAN_POINT('Ctrl Pts',(0.0973787571548163,0.104215676830788,
8.00350512245867E-17));
#18625=CARTESIAN_POINT('Ctrl Pts',(0.0914754811895955,0.108568278221023,
6.56075743842472E-17));
#18626=CARTESIAN_POINT('Ctrl Pts',(0.0852365492443714,0.11239450959967,
3.29597460435593E-17));
#18627=CARTESIAN_POINT('Ctrl Pts',(0.0787787796913796,0.116354950379705,
-7.26807264206779E-19));
#18628=CARTESIAN_POINT('Ctrl Pts',(0.0719608771003193,0.11975150351845,
7.81983513604452E-17));
#18629=CARTESIAN_POINT('Ctrl Pts',(0.0648645680501024,0.122569786811788,
1.05818132034585E-16));
#18630=CARTESIAN_POINT('Ctrl Pts',(0.0619760396963809,0.123716959397427,
1.17060669392563E-16));
#18631=CARTESIAN_POINT('Ctrl Pts',(0.0590419697559043,0.124767587801255,
-1.70921410850511E-17));
#18632=CARTESIAN_POINT('Ctrl Pts',(0.0560804949635964,0.12571697313192,
-8.67361737988404E-19));
#18633=CARTESIAN_POINT('Ctrl Pts',(0.0481895916857994,0.128246627558523,
4.23638569993146E-17));
#18634=CARTESIAN_POINT('Ctrl Pts',(0.040081547172159,0.13006877931966,2.48189907303608E-17));
#18635=CARTESIAN_POINT('Ctrl Pts',(0.0318655688619291,0.131172622122806,
0.));
#18636=CARTESIAN_POINT('Ctrl Pts',(0.0267717292715239,0.131856995664207,
-1.5387571972871E-17));
#18637=CARTESIAN_POINT('Ctrl Pts',(0.0216363184326117,0.132264755542675,
5.61228976213782E-17));
#18638=CARTESIAN_POINT('Ctrl Pts',(0.0164863123329273,0.132388468809724,
3.03576608295941E-17));
#18639=CARTESIAN_POINT('Ctrl Pts',(0.0120733572364389,0.13249447666326,
8.27985532573229E-18));
#18640=CARTESIAN_POINT('Ctrl Pts',(0.00764667637530932,0.132391154756805,
7.9933444120104E-17));
#18641=CARTESIAN_POINT('Ctrl Pts',(0.00324855819595315,0.132074892239241,
9.62771529167128E-17));
#18642=CARTESIAN_POINT('Ctrl Pts',(-0.00215998367955725,0.131685971569047,
1.16375665467493E-16));
#18643=CARTESIAN_POINT('Ctrl Pts',(-0.00753310453775717,0.130975837616781,
1.12286849362194E-16));
#18644=CARTESIAN_POINT('Ctrl Pts',(-0.0128378223015392,0.129936202211006,
1.27068494615301E-16));
#18645=CARTESIAN_POINT('Ctrl Pts',(-0.0180922709275414,0.128906418710228,
1.41710064449709E-16));
#18646=CARTESIAN_POINT('Ctrl Pts',(-0.023283936630727,0.12755123862641,
1.19281234835921E-16));
#18647=CARTESIAN_POINT('Ctrl Pts',(-0.028350637156304,0.125868914531291,
9.19403442267708E-17));
#18648=CARTESIAN_POINT('Ctrl Pts',(-0.0326437071621008,0.124443463179602,
6.87741127091605E-17));
#18649=CARTESIAN_POINT('Ctrl Pts',(-0.0368509055758185,0.122782751372096,
3.08039683582783E-17));
#18650=CARTESIAN_POINT('Ctrl Pts',(-0.0409513668396969,0.120880349084932,
-1.95156391047391E-18));
#18651=CARTESIAN_POINT('Ctrl Pts',(-0.0436523616789034,0.119627226953286,
-2.45035827619675E-17));
#18652=CARTESIAN_POINT('Ctrl Pts',(-0.0463070048384274,0.118269169850402,
-4.56986185075063E-18));
#18653=CARTESIAN_POINT('Ctrl Pts',(-0.0489111879062984,0.116810626195002,
-1.73472347597681E-18));
#18654=CARTESIAN_POINT('Ctrl Pts',(0.0958116152722397,0.0825211298936481,
0.24));
#18655=CARTESIAN_POINT('Ctrl Pts',(0.102494250906434,0.0762804363331629,
0.24));
#18656=CARTESIAN_POINT('Ctrl Pts',(0.108399952301676,0.0693089192431419,
0.24));
#18657=CARTESIAN_POINT('Ctrl Pts',(0.113520383394708,0.0617855200816623,
0.24));
#18658=CARTESIAN_POINT('Ctrl Pts',(0.11760088593285,0.0557900777417299,
0.24));
#18659=CARTESIAN_POINT('Ctrl Pts',(0.1211824537664,0.0494427873910869,0.24));
#18660=CARTESIAN_POINT('Ctrl Pts',(0.124247292533427,0.0428169095598754,
0.24));
#18661=CARTESIAN_POINT('Ctrl Pts',(0.125635784531567,0.0398151273949318,
0.24));
#18662=CARTESIAN_POINT('Ctrl Pts',(0.126914357096627,0.0367636074968772,
0.24));
#18663=CARTESIAN_POINT('Ctrl Pts',(0.128080244072735,0.0336751552254939,
0.24));
#18664=CARTESIAN_POINT('Ctrl Pts',(0.13155694143068,0.024465331227027,0.24));
#18665=CARTESIAN_POINT('Ctrl Pts',(0.134041462136676,0.0149150332268467,
0.24));
#18666=CARTESIAN_POINT('Ctrl Pts',(0.135496608205084,0.00520422800883078,
0.24));
#18667=CARTESIAN_POINT('Ctrl Pts',(0.136052940597398,0.00149158663520877,
0.24));
#18668=CARTESIAN_POINT('Ctrl Pts',(0.136458356591543,-0.00224482315054724,
0.24));
#18669=CARTESIAN_POINT('Ctrl Pts',(0.136708928272429,-0.00599574054845843,
0.24));
#18670=CARTESIAN_POINT('Ctrl Pts',(0.136894600108428,-0.00877514370161729,
0.24));
#18671=CARTESIAN_POINT('Ctrl Pts',(0.136994942037659,-0.0115613689854128,
0.24));
#18672=CARTESIAN_POINT('Ctrl Pts',(0.137008733057845,-0.0143405417274864,
0.24));
#18673=CARTESIAN_POINT('Ctrl Pts',(0.137045731231951,-0.0217964308202384,
0.24));
#18674=CARTESIAN_POINT('Ctrl Pts',(0.136462408227525,-0.0292204075226799,
0.24));
#18675=CARTESIAN_POINT('Ctrl Pts',(0.135240454646173,-0.0365388974416549,
0.24));
#18676=CARTESIAN_POINT('Ctrl Pts',(0.134058793448489,-0.0436160693529878,
0.24));
#18677=CARTESIAN_POINT('Ctrl Pts',(0.132280018312676,-0.050595007513092,
0.24));
#18678=CARTESIAN_POINT('Ctrl Pts',(0.129952822193542,-0.0574290655609092,
0.24));
#18679=CARTESIAN_POINT('Ctrl Pts',(0.128850070284018,-0.0606674134165377,
0.24));
#18680=CARTESIAN_POINT('Ctrl Pts',(0.127623182384127,-0.0638741644409745,
0.24));
#18681=CARTESIAN_POINT('Ctrl Pts',(0.126284110088584,-0.067028198101918,
0.24));
#18682=CARTESIAN_POINT('Ctrl Pts',(0.122654675969015,-0.0755769205431157,
0.24));
#18683=CARTESIAN_POINT('Ctrl Pts',(0.118195290975453,-0.0837663478860722,
0.24));
#18684=CARTESIAN_POINT('Ctrl Pts',(0.113014989178579,-0.0915013065162071,
0.24));
#18685=CARTESIAN_POINT('Ctrl Pts',(0.108985931714537,-0.0975172866704144,
0.24));
#18686=CARTESIAN_POINT('Ctrl Pts',(0.104519884911976,-0.103258562704539,
0.24));
#18687=CARTESIAN_POINT('Ctrl Pts',(0.0996546828651377,-0.108675969178894,
0.24));
#18688=CARTESIAN_POINT('Ctrl Pts',(0.0972822643803542,-0.11131765910988,
0.24));
#18689=CARTESIAN_POINT('Ctrl Pts',(0.09482095240722,-0.113875293456495,
0.24));
#18690=CARTESIAN_POINT('Ctrl Pts',(0.0922773332174137,-0.116342466058553,
0.24));
#18691=CARTESIAN_POINT('Ctrl Pts',(0.0868426048671788,-0.121613857680014,
0.24));
#18692=CARTESIAN_POINT('Ctrl Pts',(0.0810310485854155,-0.126474759557936,
0.24));
#18693=CARTESIAN_POINT('Ctrl Pts',(0.0748870600798396,-0.130870957562724,
0.24));
#18694=CARTESIAN_POINT('Ctrl Pts',(0.0715378781224404,-0.133267392228159,
0.24));
#18695=CARTESIAN_POINT('Ctrl Pts',(0.0680912231566627,-0.135524142754832,
0.24));
#18696=CARTESIAN_POINT('Ctrl Pts',(0.0645638484115253,-0.13762659390894,
0.24));
#18697=CARTESIAN_POINT('Ctrl Pts',(0.0598451535113139,-0.140439117742,0.24));
#18698=CARTESIAN_POINT('Ctrl Pts',(0.0549775790306604,-0.142978967531553,
0.24));
#18699=CARTESIAN_POINT('Ctrl Pts',(0.0499773507040556,-0.145225083935062,
0.24));
#18700=CARTESIAN_POINT('Ctrl Pts',(0.0466920976074369,-0.146700828718701,
0.24));
#18701=CARTESIAN_POINT('Ctrl Pts',(0.0433495270099635,-0.148049731670784,
0.24));
#18702=CARTESIAN_POINT('Ctrl Pts',(0.039956549802796,-0.149273502906639,
0.24));
#18703=CARTESIAN_POINT('Ctrl Pts',(-0.126296536029262,-6.10717992316628E-5,
0.159341967361942));
#18704=CARTESIAN_POINT('Ctrl Pts',(-0.12637083907321,-0.0163056929409037,
0.160361391877968));
#18705=CARTESIAN_POINT('Ctrl Pts',(-0.12344809088261,-0.0325245895549842,
0.161380816393994));
#18706=CARTESIAN_POINT('Ctrl Pts',(-0.117399968681154,-0.0474794518833934,
0.162400240910021));
#18707=CARTESIAN_POINT('Ctrl Pts',(-0.102053636235694,-0.0854254922118417,
0.164986899546353));
#18708=CARTESIAN_POINT('Ctrl Pts',(-0.0665853528586453,-0.115233359066084,
0.167573558182686));
#18709=CARTESIAN_POINT('Ctrl Pts',(-0.0265641275910804,-0.123819689910512,
0.170160216819019));
#18710=CARTESIAN_POINT('Ctrl Pts',(0.0134570976764845,-0.13240602075494,
0.172746875455351));
#18711=CARTESIAN_POINT('Ctrl Pts',(0.058031264834566,-0.119770815589554,
0.175333534091684));
#18712=CARTESIAN_POINT('Ctrl Pts',(0.0875924985281064,-0.0914586003428122,
0.177920192728017));
#18713=CARTESIAN_POINT('Ctrl Pts',(0.117153732221647,-0.0631463850960709,
0.180506851364349));
#18714=CARTESIAN_POINT('Ctrl Pts',(0.131702032450646,-0.0191571597679751,
0.183093510000682));
#18715=CARTESIAN_POINT('Ctrl Pts',(0.124851119980295,0.0211965060081854,
0.185680168637015));
#18716=CARTESIAN_POINT('Ctrl Pts',(0.118000207509943,0.0615501717843459,
0.188266827273347));
#18717=CARTESIAN_POINT('Ctrl Pts',(0.0897500823402403,0.0982682780085711,
0.19085348590968));
#18718=CARTESIAN_POINT('Ctrl Pts',(0.0525017161220023,0.115239608835997,
0.193440144546013));
#18719=CARTESIAN_POINT('Ctrl Pts',(0.0152533499037644,0.132210939663423,
0.196026803182345));
#18720=CARTESIAN_POINT('Ctrl Pts',(-0.030993257363009,0.129435495094051,
0.198613461818678));
#18721=CARTESIAN_POINT('Ctrl Pts',(-0.0659388717692058,0.108119484364762,
0.20120012045501));
#18722=CARTESIAN_POINT('Ctrl Pts',(-0.100884486175403,0.0868034736354726,
0.203786779091343));
#18723=CARTESIAN_POINT('Ctrl Pts',(-0.124529107721023,0.0469468967462671,
0.206373437727676));
#18724=CARTESIAN_POINT('Ctrl Pts',(-0.126492123469331,0.00606801008988057,
0.208960096364008));
#18725=CARTESIAN_POINT('Ctrl Pts',(-0.126588724127832,0.00405634646811867,
0.209087386696653));
#18726=CARTESIAN_POINT('Ctrl Pts',(-0.126632819376787,0.00204220716288977,
0.209214677029297));
#18727=CARTESIAN_POINT('Ctrl Pts',(-0.126625441102054,2.7778768752873E-5,
0.209341967361942));
#18728=CARTESIAN_POINT('Ctrl Pts',(-0.0398513841857245,-0.149064942821851,
0.24));
#18729=CARTESIAN_POINT('Ctrl Pts',(-0.0883048112969314,-0.136111285829332,
0.237413341363667));
#18730=CARTESIAN_POINT('Ctrl Pts',(-0.170871437255804,-0.0596187094618861,
0.232240024091002));
#18731=CARTESIAN_POINT('Ctrl Pts',(-0.145169204726118,0.108307533342445,
0.224480048182004));
#18732=CARTESIAN_POINT('Ctrl Pts',(0.00818767200092134,0.180778621679153,
0.216720072273006));
#18733=CARTESIAN_POINT('Ctrl Pts',(0.154249898498561,0.0947283641859207,
0.208960096364008));
#18734=CARTESIAN_POINT('Ctrl Pts',(0.164950538597243,-0.0745810526211722,
0.201200120455011));
#18735=CARTESIAN_POINT('Ctrl Pts',(0.0308106631569891,-0.178364693496558,
0.193440144546012));
#18736=CARTESIAN_POINT('Ctrl Pts',(-0.13036283225522,-0.125587074703769,
0.185680168637015));
#18737=CARTESIAN_POINT('Ctrl Pts',(-0.17709781441264,0.03745832727601,0.177920192728017));
#18738=CARTESIAN_POINT('Ctrl Pts',(-0.0683530255288039,0.167611467503216,
0.170160216819019));
#18739=CARTESIAN_POINT('Ctrl Pts',(0.100397202365132,0.150621028353064,
0.162400240910021));
#18740=CARTESIAN_POINT('Ctrl Pts',(0.18100910679194,0.00139719974911195,
0.154640265001023));
#18741=CARTESIAN_POINT('Ctrl Pts',(0.102711092909207,-0.149052183789333,
0.146880289092025));
#18742=CARTESIAN_POINT('Ctrl Pts',(-0.0657574679958034,-0.168648048308422,
0.139120313183027));
#18743=CARTESIAN_POINT('Ctrl Pts',(-0.176497206835689,-0.0401861834345609,
0.131360337274029));
#18744=CARTESIAN_POINT('Ctrl Pts',(-0.132288575936487,0.123555290563421,
0.123600361365031));
#18745=CARTESIAN_POINT('Ctrl Pts',(0.0280571680938306,0.178826694862324,
0.115840385456033));
#18746=CARTESIAN_POINT('Ctrl Pts',(0.163771354656592,0.0771047007047774,
0.108080409547035));
#18747=CARTESIAN_POINT('Ctrl Pts',(0.155709331479018,-0.0923080778690166,
0.100320433638038));
#18748=CARTESIAN_POINT('Ctrl Pts',(0.0109489686262093,-0.180682908560435,
0.0925604577290397));
#18749=CARTESIAN_POINT('Ctrl Pts',(-0.143423754439364,-0.110434756566834,
0.0848004818200417));
#18750=CARTESIAN_POINT('Ctrl Pts',(-0.17188331593326,0.0567648465404429,
0.0770405059110439));
#18751=CARTESIAN_POINT('Ctrl Pts',(-0.0494457976037486,0.174130301808973,
0.0692805300020459));
#18752=CARTESIAN_POINT('Ctrl Pts',(0.11640175885633,0.13862511662766,0.061520554093048));
#18753=CARTESIAN_POINT('Ctrl Pts',(0.18005704388064,-0.0185795878987759,
0.0537605781840501));
#18754=CARTESIAN_POINT('Ctrl Pts',(0.0856431484406112,-0.159474177462153,
0.0460006022750521));
#18755=CARTESIAN_POINT('Ctrl Pts',(-0.0839657292871194,-0.160363143120653,
0.0382406263660544));
#18756=CARTESIAN_POINT('Ctrl Pts',(-0.179844832231877,-0.0204718628801216,
0.0304806504570563));
#18757=CARTESIAN_POINT('Ctrl Pts',(-0.117866479118068,0.137399078213474,
0.0227206745480585));
#18758=CARTESIAN_POINT('Ctrl Pts',(0.0476444145610997,0.174632482457551,
0.0149606986390605));
#18759=CARTESIAN_POINT('Ctrl Pts',(0.171219786572432,0.0585809927800803,
0.00720072273006264));
#18760=CARTESIAN_POINT('Ctrl Pts',(0.144688050375066,-0.108949473877577,
-0.000559253178935319));
#18761=CARTESIAN_POINT('Ctrl Pts',(-0.0092814439579932,-0.180735423716049,
-0.00831922908793317));
#18762=CARTESIAN_POINT('Ctrl Pts',(-0.105867686800049,-0.122947365648507,
-0.0134925463605985));
#18763=CARTESIAN_POINT('Ctrl Pts',(-0.131895903200816,-0.0800747195988904,
-0.0160792049969312));
#18764=CARTESIAN_POINT('Ctrl Pts',(-0.0374537582415196,-0.140096572423086,
0.245359734998977));
#18765=CARTESIAN_POINT('Ctrl Pts',(-0.0829920245295529,-0.127922261611689,
0.242773076362644));
#18766=CARTESIAN_POINT('Ctrl Pts',(-0.160591096949962,-0.0560317985556137,
0.237599759089979));
#18767=CARTESIAN_POINT('Ctrl Pts',(-0.13643521822445,0.101791299158848,
0.229839783180981));
#18768=CARTESIAN_POINT('Ctrl Pts',(0.00769506740980954,0.1699022237233,
0.222079807271983));
#18769=CARTESIAN_POINT('Ctrl Pts',(0.144969579481095,0.0890291096113304,
0.214319831362985));
#18770=CARTESIAN_POINT('Ctrl Pts',(0.155026424317845,-0.0700939445729984,
0.206559855453987));
#18771=CARTESIAN_POINT('Ctrl Pts',(0.0289569648011409,-0.167633527556011,
0.19879987954499));
#18772=CARTESIAN_POINT('Ctrl Pts',(-0.122519659046519,-0.118031231043151,
0.191039903635991));
#18773=CARTESIAN_POINT('Ctrl Pts',(-0.166442869216287,0.0352046776440443,
0.183279927726994));
#18774=CARTESIAN_POINT('Ctrl Pts',(-0.064240621638164,0.157527260611955,
0.175519951817996));
#18775=CARTESIAN_POINT('Ctrl Pts',(0.0943568867767351,0.141559037340679,
0.167759975908998));
#18776=CARTESIAN_POINT('Ctrl Pts',(0.170118841887737,0.00131313836865665,
0.16));
#18777=CARTESIAN_POINT('Ctrl Pts',(0.0965315639882279,-0.140084581027326,
0.152240024091002));
#18778=CARTESIAN_POINT('Ctrl Pts',(-0.0618012237018238,-0.158501476380598,
0.144480048182004));
#18779=CARTESIAN_POINT('Ctrl Pts',(-0.165878396703103,-0.0377684145673052,
0.136720072273006));
#18780=CARTESIAN_POINT('Ctrl Pts',(-0.124329541933827,0.116121687534276,
0.128960096364008));
#18781=CARTESIAN_POINT('Ctrl Pts',(0.0263691315170036,0.168067732987372,
0.12120012045501));
#18782=CARTESIAN_POINT('Ctrl Pts',(0.153918185014798,0.0724657594331675,
0.113440144546012));
#18783=CARTESIAN_POINT('Ctrl Pts',(0.146341206869619,-0.0867544378416841,
0.105680168637015));
#18784=CARTESIAN_POINT('Ctrl Pts',(0.0102902328814698,-0.169812269106107,
0.0979201927280167));
#18785=CARTESIAN_POINT('Ctrl Pts',(-0.134794781526993,-0.103790539737311,
0.0901602168190187));
#18786=CARTESIAN_POINT('Ctrl Pts',(-0.161542096774173,0.0533496359633175,
0.0824002409100209));
#18787=CARTESIAN_POINT('Ctrl Pts',(-0.0464709316213242,0.163653894581969,
0.074640265001023));
#18788=CARTESIAN_POINT('Ctrl Pts',(0.109398542213106,0.130284849835523,
0.066880289092025));
#18789=CARTESIAN_POINT('Ctrl Pts',(0.16922405906302,-0.0174617621848401,
0.0591203131830272));
#18790=CARTESIAN_POINT('Ctrl Pts',(0.0804904984426183,-0.149879543972585,
0.0513603372740291));
#18791=CARTESIAN_POINT('Ctrl Pts',(-0.0789139998409189,-0.150715025739123,
0.0436003613650314));
#18792=CARTESIAN_POINT('Ctrl Pts',(-0.169024614954586,-0.0192401899891918,
0.0358403854560333));
#18793=CARTESIAN_POINT('Ctrl Pts',(-0.110775138777956,0.12913257502003,
0.0280804095470356));
#18794=CARTESIAN_POINT('Ctrl Pts',(0.0447779273164969,0.164125861942445,
0.0203204336380375));
#18795=CARTESIAN_POINT('Ctrl Pts',(0.16091848811479,0.0550565152494576,
0.0125604577290397));
#18796=CARTESIAN_POINT('Ctrl Pts',(0.135983012131502,-0.10239461786658,
0.00480048182004171));
#18797=CARTESIAN_POINT('Ctrl Pts',(-0.00872303347143,-0.169861624730324,
-0.00295949408895612));
#18798=CARTESIAN_POINT('Ctrl Pts',(-0.0994982439886826,-0.115550337924785,
-0.00813281136162148));
#18799=CARTESIAN_POINT('Ctrl Pts',(-0.123960494032221,-0.0752570895690155,
-0.0107194699979541));
#18800=CARTESIAN_POINT('Ctrl Pts',(-0.0350561322973148,-0.13112820202432,
0.250719469997954));
#18801=CARTESIAN_POINT('Ctrl Pts',(-0.0776792377621743,-0.119733237394047,
0.248132811361621));
#18802=CARTESIAN_POINT('Ctrl Pts',(-0.150310756644121,-0.0524448876493412,
0.242959494088956));
#18803=CARTESIAN_POINT('Ctrl Pts',(-0.127701231722781,0.0952750649752511,
0.235199518179958));
#18804=CARTESIAN_POINT('Ctrl Pts',(0.00720246281869772,0.159025825767447,
0.22743954227096));
#18805=CARTESIAN_POINT('Ctrl Pts',(0.135689260463629,0.08332985503674,0.219679566361962));
#18806=CARTESIAN_POINT('Ctrl Pts',(0.145102310038447,-0.0656068365248246,
0.211919590452964));
#18807=CARTESIAN_POINT('Ctrl Pts',(0.0271032664452926,-0.156902361615465,
0.204159614543967));
#18808=CARTESIAN_POINT('Ctrl Pts',(-0.114676485837817,-0.110475387382534,
0.196399638634969));
#18809=CARTESIAN_POINT('Ctrl Pts',(-0.155787924019933,0.0329510280120788,
0.188639662725971));
#18810=CARTESIAN_POINT('Ctrl Pts',(-0.0601282177475243,0.147443053720694,
0.180879686816973));
#18811=CARTESIAN_POINT('Ctrl Pts',(0.0883165711883383,0.132497046328295,
0.173119710907975));
#18812=CARTESIAN_POINT('Ctrl Pts',(0.159228576983534,0.00122907698820117,
0.165359734998977));
#18813=CARTESIAN_POINT('Ctrl Pts',(0.0903520350672485,-0.131116978265319,
0.157599759089979));
#18814=CARTESIAN_POINT('Ctrl Pts',(-0.0578449794078444,-0.148354904452775,
0.149839783180981));
#18815=CARTESIAN_POINT('Ctrl Pts',(-0.155259586570517,-0.0353506457000499,
0.142079807271983));
#18816=CARTESIAN_POINT('Ctrl Pts',(-0.116370507931168,0.108688084505131,
0.134319831362985));
#18817=CARTESIAN_POINT('Ctrl Pts',(0.0246810949401768,0.157308771112418,
0.126559855453988));
#18818=CARTESIAN_POINT('Ctrl Pts',(0.144065015373005,0.0678268181615582,
0.118799879544989));
#18819=CARTESIAN_POINT('Ctrl Pts',(0.13697308226022,-0.0812007978143519,
0.111039903635992));
#18820=CARTESIAN_POINT('Ctrl Pts',(0.00963149713673027,-0.15894162965178,
0.103279927726994));
#18821=CARTESIAN_POINT('Ctrl Pts',(-0.126165808614623,-0.0971463229077874,
0.0955199518179957));
#18822=CARTESIAN_POINT('Ctrl Pts',(-0.151200877615086,0.0499344253861922,
0.087759975908998));
#18823=CARTESIAN_POINT('Ctrl Pts',(-0.0434960656388994,0.153177487354966,
0.08));
#18824=CARTESIAN_POINT('Ctrl Pts',(0.102395325569881,0.121944583043386,
0.072240024091002));
#18825=CARTESIAN_POINT('Ctrl Pts',(0.158391074245402,-0.0163439364709043,
0.0644800481820042));
#18826=CARTESIAN_POINT('Ctrl Pts',(0.0753378484446251,-0.140284910483017,
0.0567200722730062));
#18827=CARTESIAN_POINT('Ctrl Pts',(-0.0738622703947183,-0.141066908357593,
0.0489600963640083));
#18828=CARTESIAN_POINT('Ctrl Pts',(-0.158204397677296,-0.018008517098262,
0.0412001204550104));
#18829=CARTESIAN_POINT('Ctrl Pts',(-0.103683798437843,0.120866071826586,
0.0334401445460125));
#18830=CARTESIAN_POINT('Ctrl Pts',(0.0419114400718942,0.153619241427338,
0.0256801686370146));
#18831=CARTESIAN_POINT('Ctrl Pts',(0.150617189657149,0.051532037718835,
0.0179201927280167));
#18832=CARTESIAN_POINT('Ctrl Pts',(0.127277973887939,-0.0958397618555833,
0.0101602168190187));
#18833=CARTESIAN_POINT('Ctrl Pts',(-0.00816462298486686,-0.1589878257446,
0.00240024091002091));
#18834=CARTESIAN_POINT('Ctrl Pts',(-0.0931288011773165,-0.108153310201063,
-0.00277307636264444));
#18835=CARTESIAN_POINT('Ctrl Pts',(-0.116025084863626,-0.0704394595391406,
-0.00535973499897709));
#18836=CARTESIAN_POINT('Ctrl Pts',(-0.0326585063531099,-0.122159831625555,
0.256079204996931));
#18837=CARTESIAN_POINT('Ctrl Pts',(-0.0723664509947957,-0.111544213176404,
0.253492546360598));
#18838=CARTESIAN_POINT('Ctrl Pts',(-0.140030416338279,-0.0488579767430688,
0.248319229087933));
#18839=CARTESIAN_POINT('Ctrl Pts',(-0.118967245221113,0.0887588307916541,
0.240559253178936));
#18840=CARTESIAN_POINT('Ctrl Pts',(0.00670985822758596,0.148149427811594,
0.232799277269937));
#18841=CARTESIAN_POINT('Ctrl Pts',(0.126408941446163,0.0776306004621497,
0.225039301360939));
#18842=CARTESIAN_POINT('Ctrl Pts',(0.13517819575905,-0.0611197284766509,
0.217279325451942));
#18843=CARTESIAN_POINT('Ctrl Pts',(0.0252495680894444,-0.146171195674918,
0.209519349542944));
#18844=CARTESIAN_POINT('Ctrl Pts',(-0.106833312629116,-0.102919543721916,
0.201759373633946));
#18845=CARTESIAN_POINT('Ctrl Pts',(-0.14513297882358,0.0306973783801131,
0.193999397724948));
#18846=CARTESIAN_POINT('Ctrl Pts',(-0.0560158138568844,0.137358846829434,
0.18623942181595));
#18847=CARTESIAN_POINT('Ctrl Pts',(0.0822762555999414,0.12343505531591,
0.178479445906952));
#18848=CARTESIAN_POINT('Ctrl Pts',(0.148338312079331,0.00114501560774606,
0.170719469997954));
#18849=CARTESIAN_POINT('Ctrl Pts',(0.0841725061462688,-0.122149375503312,
0.162959494088956));
#18850=CARTESIAN_POINT('Ctrl Pts',(-0.0538887351138648,-0.138208332524951,
0.155199518179959));
#18851=CARTESIAN_POINT('Ctrl Pts',(-0.144640776437932,-0.0329328768327946,
0.14743954227096));
#18852=CARTESIAN_POINT('Ctrl Pts',(-0.108411473928508,0.101254481475986,
0.139679566361963));
#18853=CARTESIAN_POINT('Ctrl Pts',(0.0229930583633497,0.146549809237466,
0.131919590452964));
#18854=CARTESIAN_POINT('Ctrl Pts',(0.134211845731212,0.0631878768899486,
0.124159614543967));
#18855=CARTESIAN_POINT('Ctrl Pts',(0.127604957650822,-0.0756471577870196,
0.116399638634969));
#18856=CARTESIAN_POINT('Ctrl Pts',(0.00897276139199077,-0.148070990197453,
0.108639662725971));
#18857=CARTESIAN_POINT('Ctrl Pts',(-0.117536835702253,-0.0905021060782641,
0.100879686816973));
#18858=CARTESIAN_POINT('Ctrl Pts',(-0.140859658455999,0.0465192148090667,
0.0931197109079749));
#18859=CARTESIAN_POINT('Ctrl Pts',(-0.0405211996564747,0.142701080127962,
0.0853597349989771));
#18860=CARTESIAN_POINT('Ctrl Pts',(0.0953921089266558,0.113604316251249,
0.077599759089979));
#18861=CARTESIAN_POINT('Ctrl Pts',(0.147558089427783,-0.0152261107569683,
0.0698397831809813));
#18862=CARTESIAN_POINT('Ctrl Pts',(0.070185198446632,-0.130690276993449,
0.0620798072719832));
#18863=CARTESIAN_POINT('Ctrl Pts',(-0.0688105409485176,-0.131418790976063,
0.0543198313629854));
#18864=CARTESIAN_POINT('Ctrl Pts',(-0.147384180400005,-0.0167768442073323,
0.0465598554539874));
#18865=CARTESIAN_POINT('Ctrl Pts',(-0.0965924580977301,0.112599568633142,
0.0387998795449896));
#18866=CARTESIAN_POINT('Ctrl Pts',(0.0390449528272914,0.143112620912232,
0.0310399036359916));
#18867=CARTESIAN_POINT('Ctrl Pts',(0.140315891199508,0.0480075601882123,
0.0232799277269937));
#18868=CARTESIAN_POINT('Ctrl Pts',(0.118572935644375,-0.0892849058445864,
0.0155199518179958));
#18869=CARTESIAN_POINT('Ctrl Pts',(-0.00760621249830358,-0.148114026758875,
0.00775997590899793));
#18870=CARTESIAN_POINT('Ctrl Pts',(-0.0867593583659504,-0.100756282477341,
0.00258665863633259));
#18871=CARTESIAN_POINT('Ctrl Pts',(-0.108089675695031,-0.0656218295092657,
-5.55111512312578E-17));
#18872=CARTESIAN_POINT('Ctrl Pts',(-0.108089675695031,-0.0656218295092657,
-5.55111512312578E-17));
#18873=CARTESIAN_POINT('Ctrl Pts',(-0.104219465379748,-0.0739058869203245,
-4.02841154597017E-17));
#18874=CARTESIAN_POINT('Ctrl Pts',(-0.0994141168358061,-0.0816768736924768,
-5.16144647363644E-17));
#18875=CARTESIAN_POINT('Ctrl Pts',(-0.0938412360364922,-0.088871564406415,
-3.81639164714898E-17));
#18876=CARTESIAN_POINT('Ctrl Pts',(-0.0894001862863345,-0.094605040600905,
-2.74451237748006E-17));
#18877=CARTESIAN_POINT('Ctrl Pts',(-0.0844703330957707,-0.0999727304469881,
3.12377098840079E-17));
#18878=CARTESIAN_POINT('Ctrl Pts',(-0.0791158513129458,-0.104935071387697,
-1.21430643318376E-17));
#18879=CARTESIAN_POINT('Ctrl Pts',(-0.0766900604813501,-0.107183206995485,
-3.17962611543325E-17));
#18880=CARTESIAN_POINT('Ctrl Pts',(-0.0741829996358932,-0.109342173006691,
4.83248416902999E-17));
#18881=CARTESIAN_POINT('Ctrl Pts',(-0.0716059924168524,-0.111405381598006,
5.3776427755281E-17));
#18882=CARTESIAN_POINT('Ctrl Pts',(-0.0639212992135713,-0.117557915794061,
7.00331794132204E-17));
#18883=CARTESIAN_POINT('Ctrl Pts',(-0.0556061968393146,-0.12287204611112,
-5.69073736333764E-18));
#18884=CARTESIAN_POINT('Ctrl Pts',(-0.0468203466856493,-0.127256781127915,
5.55111512312578E-17));
#18885=CARTESIAN_POINT('Ctrl Pts',(-0.0434613267337519,-0.12893315986732,
7.89099528597243E-17));
#18886=CARTESIAN_POINT('Ctrl Pts',(-0.0400330653128497,-0.130473352587733,
3.97002991909352E-17));
#18887=CARTESIAN_POINT('Ctrl Pts',(-0.0365431560942257,-0.131870761756357,
6.59194920871187E-17));
#18888=CARTESIAN_POINT('Ctrl Pts',(-0.0339571636773035,-0.13290622981212,
8.5347686277821E-17));
#18889=CARTESIAN_POINT('Ctrl Pts',(-0.0313383144727484,-0.133862652235137,
-2.74403076010104E-17));
#18890=CARTESIAN_POINT('Ctrl Pts',(-0.0286994266230122,-0.134734580282325,
-2.42861286636753E-17));
#18891=CARTESIAN_POINT('Ctrl Pts',(-0.0216199050576346,-0.137073760181214,
-1.58242011095522E-17));
#18892=CARTESIAN_POINT('Ctrl Pts',(-0.0143790427459088,-0.138813119073991,
5.80198461902811E-17));
#18893=CARTESIAN_POINT('Ctrl Pts',(-0.0070411538297537,-0.139912507657099,
6.93889390390723E-17));
#18894=CARTESIAN_POINT('Ctrl Pts',(5.47883476400097E-5,-0.140975646920361,
8.02325614020808E-17));
#18895=CARTESIAN_POINT('Ctrl Pts',(0.00724182591717642,-0.141440539972256,
1.32011341321413E-16));
#18896=CARTESIAN_POINT('Ctrl Pts',(0.0144605478337719,-0.141339082434075,
1.61329283265843E-16));
#18897=CARTESIAN_POINT('Ctrl Pts',(0.0178811722145177,-0.141291006315792,
1.75221724083914E-16));
#18898=CARTESIAN_POINT('Ctrl Pts',(0.021310106848269,-0.141115105569205,
1.85534911235541E-16));
#18899=CARTESIAN_POINT('Ctrl Pts',(0.0247235715439624,-0.140816220288761,
1.71737624121704E-16));
#18900=CARTESIAN_POINT('Ctrl Pts',(0.0339754553361668,-0.140006119078294,
1.34341339582434E-16));
#18901=CARTESIAN_POINT('Ctrl Pts',(0.0431421008898472,-0.138295657968001,
8.04496487960062E-17));
#18902=CARTESIAN_POINT('Ctrl Pts',(0.0520992976556894,-0.135759125106636,
3.20923843055709E-17));
#18903=CARTESIAN_POINT('Ctrl Pts',(0.0590658916121619,-0.13378629867842,
-5.518202506064E-18));
#18904=CARTESIAN_POINT('Ctrl Pts',(0.0659062642374416,-0.131312982137409,
7.87850579480063E-17));
#18905=CARTESIAN_POINT('Ctrl Pts',(0.0725619642951071,-0.128359965266718,
7.63278329429795E-17));
#18906=CARTESIAN_POINT('Ctrl Pts',(0.0758074813473741,-0.126919986522721,
7.51296170399226E-17));
#18907=CARTESIAN_POINT('Ctrl Pts',(0.0790005264283722,-0.125369490597537,
8.38688896655138E-17));
#18908=CARTESIAN_POINT('Ctrl Pts',(0.0821329715644795,-0.123712761836801,
7.24247051220317E-17));
#18909=CARTESIAN_POINT('Ctrl Pts',(0.0888257654942848,-0.120172989003949,
4.79730178566093E-17));
#18910=CARTESIAN_POINT('Ctrl Pts',(0.0952446087626691,-0.116147988031934,
8.96774285244103E-17));
#18911=CARTESIAN_POINT('Ctrl Pts',(0.101324221742587,-0.111663228753314,
8.28330459778925E-17));
#18912=CARTESIAN_POINT('Ctrl Pts',(0.104638321741973,-0.109218510516871,
7.91020571356516E-17));
#18913=CARTESIAN_POINT('Ctrl Pts',(0.107849695272814,-0.106637925639498,
3.17151869302413E-17));
#18914=CARTESIAN_POINT('Ctrl Pts',(0.110939265073957,-0.10393289123317,
1.53956708492942E-17));
#18915=CARTESIAN_POINT('Ctrl Pts',(0.115072333360666,-0.100314234708527,
-6.43574216607592E-18));
#18916=CARTESIAN_POINT('Ctrl Pts',(0.118992075260627,-0.0964697210975667,
5.54296751400654E-17));
#18917=CARTESIAN_POINT('Ctrl Pts',(0.122673447199167,-0.0924082746861152,
3.52365706057789E-17));
#18918=CARTESIAN_POINT('Ctrl Pts',(0.125092164655522,-0.0897398425098966,
2.31620156359627E-17));
#18919=CARTESIAN_POINT('Ctrl Pts',(0.127407959881093,-0.0869777021544565,
-4.01489640485901E-17));
#18920=CARTESIAN_POINT('Ctrl Pts',(0.129620323775263,-0.0841289546921697,
-3.98986399474666E-17));
#18921=CARTESIAN_POINT('Ctrl Pts',(-0.126471935391749,0.000101176582396995,
0.195658032638058));
#18922=CARTESIAN_POINT('Ctrl Pts',(-0.126547267107008,0.00888033934128026,
0.195105154333688));
#18923=CARTESIAN_POINT('Ctrl Pts',(-0.125707148272093,0.0176451944231377,
0.194552276029318));
#18924=CARTESIAN_POINT('Ctrl Pts',(-0.12389684029672,0.0262048027713284,
0.193999397724948));
#18925=CARTESIAN_POINT('Ctrl Pts',(-0.115427257168015,0.0662512011965534,
0.191412739088615));
#18926=CARTESIAN_POINT('Ctrl Pts',(-0.0857215355124495,0.101805024012994,
0.188826080452282));
#18927=CARTESIAN_POINT('Ctrl Pts',(-0.0478199964418627,0.117261303502293,
0.18623942181595));
#18928=CARTESIAN_POINT('Ctrl Pts',(-0.0099184573712758,0.132717582991593,
0.183652763179617));
#18929=CARTESIAN_POINT('Ctrl Pts',(0.0361788991143328,0.128076319153751,
0.181066104543285));
#18930=CARTESIAN_POINT('Ctrl Pts',(0.070237920103702,0.105374013950137,
0.178479445906952));
#18931=CARTESIAN_POINT('Ctrl Pts',(0.104296941093071,0.0826717087465222,
0.175892787270619));
#18932=CARTESIAN_POINT('Ctrl Pts',(0.126317626586201,0.0419083621771342,
0.173306128634287));
#18933=CARTESIAN_POINT('Ctrl Pts',(0.126633668343922,0.000977623707263797,
0.170719469997954));
#18934=CARTESIAN_POINT('Ctrl Pts',(0.126949710101644,-0.0399531147626067,
0.168132811361621));
#18935=CARTESIAN_POINT('Ctrl Pts',(0.105561108123956,-0.08105124513296,
0.165546152725289));
#18936=CARTESIAN_POINT('Ctrl Pts',(0.0718566002584231,-0.104276803155076,
0.162959494088956));
#18937=CARTESIAN_POINT('Ctrl Pts',(0.0381520923928904,-0.127502361177192,
0.160372835452623));
#18938=CARTESIAN_POINT('Ctrl Pts',(-0.00786832136048696,-0.132855346851071,
0.157786176816291));
#18939=CARTESIAN_POINT('Ctrl Pts',(-0.0460038684578537,-0.117985930405985,
0.155199518179958));
#18940=CARTESIAN_POINT('Ctrl Pts',(-0.0841394155552204,-0.103116513960899,
0.152612859543626));
#18941=CARTESIAN_POINT('Ctrl Pts',(-0.114390095996576,-0.0680246953968468,
0.150026200907293));
#18942=CARTESIAN_POINT('Ctrl Pts',(-0.12347721913235,-0.0281142263966907,
0.14743954227096));
#18943=CARTESIAN_POINT('Ctrl Pts',(-0.125563410841138,-0.018951712774069,
0.14684570572666));
#18944=CARTESIAN_POINT('Ctrl Pts',(-0.126534167537385,-0.00953522996602069,
0.146251869182359));
#18945=CARTESIAN_POINT('Ctrl Pts',(-0.126453631260982,-0.000102348163238207,
0.145658032638058));
#18946=CARTESIAN_POINT('Ctrl Pts',(-0.0398513841857245,-0.149064942821851,
0.24));
#18947=CARTESIAN_POINT('Ctrl Pts',(-0.0498806325786677,-0.145400296738327,
0.24));
#18948=CARTESIAN_POINT('Ctrl Pts',(-0.0594363948008725,-0.140639648297949,
0.24));
#18949=CARTESIAN_POINT('Ctrl Pts',(-0.0684062055177017,-0.134931499399492,
0.24));
#18950=CARTESIAN_POINT('Ctrl Pts',(-0.0735915624001909,-0.131631676235849,
0.24));
#18951=CARTESIAN_POINT('Ctrl Pts',(-0.0785806353345173,-0.128014298080738,
0.24));
#18952=CARTESIAN_POINT('Ctrl Pts',(-0.0833462611484583,-0.124102693747304,
0.24));
#18953=CARTESIAN_POINT('Ctrl Pts',(-0.0858656342542594,-0.122034803580736,
0.24));
#18954=CARTESIAN_POINT('Ctrl Pts',(-0.0883241156266364,-0.11988309220465,
0.24));
#18955=CARTESIAN_POINT('Ctrl Pts',(-0.0907117892851122,-0.117655751751618,
0.24));
#18956=CARTESIAN_POINT('Ctrl Pts',(-0.0983819858496404,-0.110500611839494,
0.24));
#18957=CARTESIAN_POINT('Ctrl Pts',(-0.105284458416918,-0.102606966330569,
0.24));
#18958=CARTESIAN_POINT('Ctrl Pts',(-0.111294422020379,-0.0941015332659665,
0.24));
#18959=CARTESIAN_POINT('Ctrl Pts',(-0.114410577497229,-0.0896914812962706,
0.24));
#18960=CARTESIAN_POINT('Ctrl Pts',(-0.117286101138547,-0.0851164738413172,
0.24));
#18961=CARTESIAN_POINT('Ctrl Pts',(-0.119898298320422,-0.0803922539627851,
0.24));
#18962=CARTESIAN_POINT('Ctrl Pts',(-0.1222721977331,-0.0760990011896685,
0.24));
#18963=CARTESIAN_POINT('Ctrl Pts',(-0.124430744329062,-0.0716759619599862,
0.24));
#18964=CARTESIAN_POINT('Ctrl Pts',(-0.126341093034125,-0.0671690272221462,
0.24));
#18965=CARTESIAN_POINT('Ctrl Pts',(-0.129206708925078,-0.060408406100978,
0.24));
#18966=CARTESIAN_POINT('Ctrl Pts',(-0.131522065955468,-0.0534490321795157,
0.24));
#18967=CARTESIAN_POINT('Ctrl Pts',(-0.133233091500091,-0.0463330844490581,
0.24));
#18968=CARTESIAN_POINT('Ctrl Pts',(-0.135004134506116,-0.0389675313754268,
0.24));
#18969=CARTESIAN_POINT('Ctrl Pts',(-0.136127599829873,-0.0314337185245799,
0.24));
#18970=CARTESIAN_POINT('Ctrl Pts',(-0.136615064298196,-0.0238138180582873,
0.24));
#18971=CARTESIAN_POINT('Ctrl Pts',(-0.136813484749433,-0.0207121682209076,
0.24));
#18972=CARTESIAN_POINT('Ctrl Pts',(-0.136906013213758,-0.0175970392000076,
0.24));
#18973=CARTESIAN_POINT('Ctrl Pts',(-0.136893785357156,-0.0144871321155608,
0.24));
#18974=CARTESIAN_POINT('Ctrl Pts',(-0.136861203984761,-0.00620072149302863,
0.24));
#18975=CARTESIAN_POINT('Ctrl Pts',(-0.136088646936857,0.00207357465703332,
0.24));
#18976=CARTESIAN_POINT('Ctrl Pts',(-0.134599584032292,0.0102285531249486,
0.24));
#18977=CARTESIAN_POINT('Ctrl Pts',(-0.133676409755049,0.0152843948425598,
0.24));
#18978=CARTESIAN_POINT('Ctrl Pts',(-0.132477333465274,0.0202942984003417,
0.24));
#18979=CARTESIAN_POINT('Ctrl Pts',(-0.131003622030167,0.0252303138624672,
0.24));
#18980=CARTESIAN_POINT('Ctrl Pts',(-0.129740734874544,0.029460199292259,
0.24));
#18981=CARTESIAN_POINT('Ctrl Pts',(-0.128274507607502,0.0336384499732856,
0.24));
#18982=CARTESIAN_POINT('Ctrl Pts',(-0.126614574688298,0.0377237273426867,
0.24));
#18983=CARTESIAN_POINT('Ctrl Pts',(-0.124573382985647,0.042747324485064,
0.24));
#18984=CARTESIAN_POINT('Ctrl Pts',(-0.122237651925267,0.0476379767326878,
0.24));
#18985=CARTESIAN_POINT('Ctrl Pts',(-0.119609691052418,0.0523617558795304,
0.24));
#18986=CARTESIAN_POINT('Ctrl Pts',(-0.117006563775536,0.0570408964535612,
0.24));
#18987=CARTESIAN_POINT('Ctrl Pts',(-0.114113358229268,0.0615597689541448,
0.24));
#18988=CARTESIAN_POINT('Ctrl Pts',(-0.110947628485839,0.0658586917144141,
0.24));
#18989=CARTESIAN_POINT('Ctrl Pts',(-0.108265305855902,0.0695011687224882,
0.24));
#18990=CARTESIAN_POINT('Ctrl Pts',(-0.105385772272888,0.0729892759232728,
0.24));
#18991=CARTESIAN_POINT('Ctrl Pts',(-0.102309360287629,0.0763011815833395,
0.24));
#18992=CARTESIAN_POINT('Ctrl Pts',(-0.100282916666232,0.0784827457339379,
0.24));
#18993=CARTESIAN_POINT('Ctrl Pts',(-0.0981709975111385,0.0805877996091198,
0.24));
#18994=CARTESIAN_POINT('Ctrl Pts',(-0.0959791030802606,0.0826138105732947,
0.24));
#18995=CARTESIAN_POINT('Origin',(0.,0.,0.24));
#18996=CARTESIAN_POINT('',(0.158771324027147,-0.275,0.24));
#18997=CARTESIAN_POINT('',(0.317542648054294,0.,0.24));
#18998=CARTESIAN_POINT('',(0.158771324027147,-0.275,0.24));
#18999=CARTESIAN_POINT('',(0.158771324027147,0.275,0.24));
#19000=CARTESIAN_POINT('',(0.317542648054294,0.,0.24));
#19001=CARTESIAN_POINT('',(-0.158771324027147,0.275,0.24));
#19002=CARTESIAN_POINT('',(0.158771324027147,0.275,0.24));
#19003=CARTESIAN_POINT('',(-0.317542648054294,5.55111512312578E-17,0.24));
#19004=CARTESIAN_POINT('',(-0.158771324027147,0.275,0.24));
#19005=CARTESIAN_POINT('',(-0.158771324027147,-0.275,0.24));
#19006=CARTESIAN_POINT('',(-0.317542648054294,3.88877587532466E-17,0.24));
#19007=CARTESIAN_POINT('',(-0.158771324027147,-0.275,0.24));
#19008=CARTESIAN_POINT('Origin',(0.,0.,0.12));
#19009=CARTESIAN_POINT('Origin',(-0.158771324027147,-0.275,0.));
#19010=CARTESIAN_POINT('',(-0.158771324027147,-0.275,0.));
#19011=CARTESIAN_POINT('',(0.158771324027147,-0.275,0.));
#19012=CARTESIAN_POINT('',(-0.158771324027147,-0.275,0.));
#19013=CARTESIAN_POINT('',(0.158771324027147,-0.275,0.));
#19014=CARTESIAN_POINT('',(-0.158771324027147,-0.275,0.));
#19015=CARTESIAN_POINT('Origin',(-0.317542648054294,3.88877587532466E-17,
0.));
#19016=CARTESIAN_POINT('',(-0.317542648054294,3.88877587532466E-17,0.));
#19017=CARTESIAN_POINT('',(-0.317542648054294,3.88877587532466E-17,0.));
#19018=CARTESIAN_POINT('',(-0.317542648054294,3.88877587532466E-17,0.));
#19019=CARTESIAN_POINT('Origin',(-0.158771324027147,0.275,0.));
#19020=CARTESIAN_POINT('',(-0.158771324027147,0.275,0.));
#19021=CARTESIAN_POINT('',(-0.158771324027147,0.275,0.));
#19022=CARTESIAN_POINT('',(-0.158771324027147,0.275,0.));
#19023=CARTESIAN_POINT('Origin',(0.158771324027147,0.275,0.));
#19024=CARTESIAN_POINT('',(0.158771324027147,0.275,0.));
#19025=CARTESIAN_POINT('',(0.158771324027147,0.275,0.));
#19026=CARTESIAN_POINT('',(0.158771324027147,0.275,0.));
#19027=CARTESIAN_POINT('Origin',(0.317542648054294,0.,0.));
#19028=CARTESIAN_POINT('',(0.317542648054294,0.,0.));
#19029=CARTESIAN_POINT('',(0.317542648054294,0.,0.));
#19030=CARTESIAN_POINT('',(0.317542648054294,0.,0.));
#19031=CARTESIAN_POINT('Origin',(0.158771324027147,-0.275,0.));
#19032=CARTESIAN_POINT('',(0.158771324027147,-0.275,0.));
#19033=CARTESIAN_POINT('Origin',(0.,0.,0.));
#19075=UNCERTAINTY_MEASURE_WITH_UNIT(LENGTH_MEASURE(0.001),#19091,
'DISTANCE_ACCURACY_VALUE',
'Maximum model space distance between geometric entities at asserted c
onnectivities');
#19077=UNCERTAINTY_MEASURE_WITH_UNIT(LENGTH_MEASURE(0.001),#19091,
'DISTANCE_ACCURACY_VALUE',
'Maximum model space distance between geometric entities at asserted c
onnectivities');
#19088=(
GEOMETRIC_REPRESENTATION_CONTEXT(3)
GLOBAL_UNCERTAINTY_ASSIGNED_CONTEXT((#19075))
GLOBAL_UNIT_ASSIGNED_CONTEXT((#19091,#19093,#19094))
REPRESENTATION_CONTEXT('','3D')
);
#19090=(
GEOMETRIC_REPRESENTATION_CONTEXT(3)
GLOBAL_UNCERTAINTY_ASSIGNED_CONTEXT((#19077))
GLOBAL_UNIT_ASSIGNED_CONTEXT((#19091,#19093,#19094))
REPRESENTATION_CONTEXT('','3D')
);
#19091=(
LENGTH_UNIT()
NAMED_UNIT(*)
SI_UNIT(.CENTI.,.METRE.)
);
#19093=(
NAMED_UNIT(*)
PLANE_ANGLE_UNIT()
SI_UNIT($,.RADIAN.)
);
#19094=(
NAMED_UNIT(*)
SI_UNIT($,.STERADIAN.)
SOLID_ANGLE_UNIT()
);
#19105=SHAPE_DEFINITION_REPRESENTATION(#19117,#19145);
#19117=PRODUCT_DEFINITION_SHAPE('',$,#19158);
#19145=SHAPE_REPRESENTATION('',(#7386),#19088);
#19147=PRODUCT_DEFINITION_CONTEXT('part definition',#19185,'design');
#19158=PRODUCT_DEFINITION('2026-11-10-05-09-19-267','Hex nut M3',#19170,
#19147);
#19170=PRODUCT_DEFINITION_FORMATION('',$,#19197);
#19185=APPLICATION_CONTEXT(
'Core Data for Automotive Mechanical Design Process');
#19186=PRODUCT_CONTEXT('part definition',#19185,'mechanical');
#19197=PRODUCT('2026-11-10-05-09-19-267','Hex nut M3',$,(#19186));
#19205=PRESENTATION_STYLE_ASSIGNMENT((#19213));
#19213=SURFACE_STYLE_USAGE(.BOTH.,#19221);
#19221=SURFACE_SIDE_STYLE('',(#19229));
#19229=SURFACE_STYLE_FILL_AREA(#19237);
#19237=FILL_AREA_STYLE('Fastener gray',(#19245));
#19245=FILL_AREA_STYLE_COLOUR('Fastener gray',#19253);
#19253=COLOUR_RGB('Fastener gray',0.607843137254902,0.643137254901961,0.698039215686274);
ENDSEC;
END-ISO-10303-21;
